ISO-10303-21;
HEADER;
/* Generated by software containing ST-Developer
 * from STEP Tools, Inc. (www.steptools.com) 
 */

FILE_DESCRIPTION(
/* description */ (''),
/* implementation_level */ '2;1');

FILE_NAME(
/* name */ 'Slider_02 (1).step',
/* time_stamp */ '2026-10-22T15:07:41+06:00',
/* author */ (''),
/* organization */ (''),
/* preprocessor_version */ 'ST-DEVELOPER v20.2',
/* originating_system */ 'Autodesk Translation Framework v15.15.0.0',
/* authorisation */ '');

FILE_SCHEMA (('AUTOMOTIVE_DESIGN { 1 0 10303 214 3 1 1 }'));
ENDSEC;

DATA;
#10=MECHANICAL_DESIGN_GEOMETRIC_PRESENTATION_REPRESENTATION('',(#2890),#19220);
#79=SHAPE_REPRESENTATION_RELATIONSHIP('SRR','None',#19282,#93);
#93=ADVANCED_BREP_SHAPE_REPRESENTATION('',(#107),#19218);
#107=MANIFOLD_SOLID_BREP('Slider_02',#11326);
#622=FACE_BOUND('',#4487,.T.);
#623=FACE_BOUND('',#4489,.T.);
#805=PLANE('',#12628);
#806=PLANE('',#12632);
#807=PLANE('',#12633);
#808=PLANE('',#12637);
#809=PLANE('',#12644);
#810=PLANE('',#12645);
#811=PLANE('',#12649);
#812=PLANE('',#12650);
#813=PLANE('',#12654);
#814=PLANE('',#12658);
#815=PLANE('',#12662);
#816=PLANE('',#12663);
#817=PLANE('',#12664);
#818=PLANE('',#12668);
#819=PLANE('',#12672);
#820=PLANE('',#12673);
#821=PLANE('',#12674);
#822=PLANE('',#12678);
#823=PLANE('',#12682);
#824=PLANE('',#12686);
#825=PLANE('',#12690);
#826=PLANE('',#12691);
#827=PLANE('',#12692);
#828=PLANE('',#12696);
#829=PLANE('',#12700);
#830=PLANE('',#12701);
#1587=LINE('',#18891,#2442);
#1588=LINE('',#18893,#2443);
#1589=LINE('',#18895,#2444);
#1590=LINE('',#18896,#2445);
#1591=LINE('',#18901,#2446);
#1592=LINE('',#18905,#2447);
#1593=LINE('',#18907,#2448);
#1594=LINE('',#18908,#2449);
#1595=LINE('',#18912,#2450);
#1596=LINE('',#18914,#2451);
#1597=LINE('',#18916,#2452);
#1598=LINE('',#18917,#2453);
#1599=LINE('',#18922,#2454);
#1600=LINE('',#18926,#2455);
#1601=LINE('',#18928,#2456);
#1602=LINE('',#18929,#2457);
#1603=LINE('',#18934,#2458);
#1604=LINE('',#18941,#2459);
#1605=LINE('',#18944,#2460);
#1606=LINE('',#18946,#2461);
#1607=LINE('',#18947,#2462);
#1608=LINE('',#18951,#2463);
#1609=LINE('',#18953,#2464);
#1610=LINE('',#18955,#2465);
#1611=LINE('',#18956,#2466);
#1612=LINE('',#18962,#2467);
#1613=LINE('',#18965,#2468);
#1614=LINE('',#18967,#2469);
#1615=LINE('',#18968,#2470);
#1616=LINE('',#18972,#2471);
#1617=LINE('',#18974,#2472);
#1618=LINE('',#18976,#2473);
#1619=LINE('',#18977,#2474);
#1620=LINE('',#18983,#2475);
#1621=LINE('',#18986,#2476);
#1622=LINE('',#18988,#2477);
#1623=LINE('',#18989,#2478);
#1624=LINE('',#18995,#2479);
#1625=LINE('',#18997,#2480);
#1626=LINE('',#18998,#2481);
#1627=LINE('',#19004,#2482);
#1628=LINE('',#19006,#2483);
#1629=LINE('',#19007,#2484);
#1630=LINE('',#19010,#2485);
#1631=LINE('',#19012,#2486);
#1632=LINE('',#19013,#2487);
#1633=LINE('',#19015,#2488);
#1634=LINE('',#19016,#2489);
#1635=LINE('',#19021,#2490);
#1636=LINE('',#19025,#2491);
#1637=LINE('',#19027,#2492);
#1638=LINE('',#19028,#2493);
#1639=LINE('',#19033,#2494);
#1640=LINE('',#19037,#2495);
#1641=LINE('',#19039,#2496);
#1642=LINE('',#19040,#2497);
#1643=LINE('',#19043,#2498);
#1644=LINE('',#19045,#2499);
#1645=LINE('',#19046,#2500);
#1646=LINE('',#19049,#2501);
#1647=LINE('',#19051,#2502);
#1648=LINE('',#19052,#2503);
#1649=LINE('',#19057,#2504);
#1650=LINE('',#19061,#2505);
#1651=LINE('',#19063,#2506);
#1652=LINE('',#19064,#2507);
#1653=LINE('',#19069,#2508);
#1654=LINE('',#19073,#2509);
#1655=LINE('',#19075,#2510);
#1656=LINE('',#19076,#2511);
#1657=LINE('',#19082,#2512);
#1658=LINE('',#19085,#2513);
#1659=LINE('',#19087,#2514);
#1660=LINE('',#19088,#2515);
#1661=LINE('',#19094,#2516);
#1662=LINE('',#19097,#2517);
#1663=LINE('',#19099,#2518);
#1664=LINE('',#19100,#2519);
#1665=LINE('',#19103,#2520);
#1666=LINE('',#19105,#2521);
#1667=LINE('',#19106,#2522);
#1668=LINE('',#19109,#2523);
#1669=LINE('',#19111,#2524);
#1670=LINE('',#19112,#2525);
#1671=LINE('',#19118,#2526);
#1672=LINE('',#19121,#2527);
#1673=LINE('',#19123,#2528);
#1674=LINE('',#19124,#2529);
#2442=VECTOR('',#15768,10.);
#2443=VECTOR('',#15769,10.);
#2444=VECTOR('',#15770,10.);
#2445=VECTOR('',#15771,10.);
#2446=VECTOR('',#15776,10.);
#2447=VECTOR('',#15781,10.);
#2448=VECTOR('',#15782,10.);
#2449=VECTOR('',#15783,10.);
#2450=VECTOR('',#15786,10.);
#2451=VECTOR('',#15787,10.);
#2452=VECTOR('',#15788,10.);
#2453=VECTOR('',#15789,10.);
#2454=VECTOR('',#15794,10.);
#2455=VECTOR('',#15799,10.);
#2456=VECTOR('',#15800,10.);
#2457=VECTOR('',#15801,10.);
#2458=VECTOR('',#15806,10.);
#2459=VECTOR('',#15815,10.);
#2460=VECTOR('',#15818,10.);
#2461=VECTOR('',#15819,10.);
#2462=VECTOR('',#15820,10.);
#2463=VECTOR('',#15823,10.);
#2464=VECTOR('',#15824,10.);
#2465=VECTOR('',#15825,10.);
#2466=VECTOR('',#15826,10.);
#2467=VECTOR('',#15833,10.);
#2468=VECTOR('',#15836,10.);
#2469=VECTOR('',#15837,10.);
#2470=VECTOR('',#15838,10.);
#2471=VECTOR('',#15841,10.);
#2472=VECTOR('',#15842,10.);
#2473=VECTOR('',#15843,10.);
#2474=VECTOR('',#15844,10.);
#2475=VECTOR('',#15851,10.);
#2476=VECTOR('',#15854,10.);
#2477=VECTOR('',#15855,10.);
#2478=VECTOR('',#15856,10.);
#2479=VECTOR('',#15865,10.);
#2480=VECTOR('',#15866,10.);
#2481=VECTOR('',#15867,10.);
#2482=VECTOR('',#15876,10.);
#2483=VECTOR('',#15877,10.);
#2484=VECTOR('',#15878,10.);
#2485=VECTOR('',#15881,10.);
#2486=VECTOR('',#15882,10.);
#2487=VECTOR('',#15883,10.);
#2488=VECTOR('',#15886,10.);
#2489=VECTOR('',#15887,10.);
#2490=VECTOR('',#15892,10.);
#2491=VECTOR('',#15897,10.);
#2492=VECTOR('',#15898,10.);
#2493=VECTOR('',#15899,10.);
#2494=VECTOR('',#15904,10.);
#2495=VECTOR('',#15909,10.);
#2496=VECTOR('',#15910,10.);
#2497=VECTOR('',#15911,10.);
#2498=VECTOR('',#15914,10.);
#2499=VECTOR('',#15915,10.);
#2500=VECTOR('',#15916,10.);
#2501=VECTOR('',#15919,10.);
#2502=VECTOR('',#15920,10.);
#2503=VECTOR('',#15921,10.);
#2504=VECTOR('',#15926,10.);
#2505=VECTOR('',#15931,10.);
#2506=VECTOR('',#15932,10.);
#2507=VECTOR('',#15933,10.);
#2508=VECTOR('',#15938,10.);
#2509=VECTOR('',#15943,10.);
#2510=VECTOR('',#15944,10.);
#2511=VECTOR('',#15945,10.);
#2512=VECTOR('',#15952,10.);
#2513=VECTOR('',#15955,10.);
#2514=VECTOR('',#15956,10.);
#2515=VECTOR('',#15957,10.);
#2516=VECTOR('',#15964,10.);
#2517=VECTOR('',#15967,10.);
#2518=VECTOR('',#15968,10.);
#2519=VECTOR('',#15969,10.);
#2520=VECTOR('',#15972,10.);
#2521=VECTOR('',#15973,10.);
#2522=VECTOR('',#15974,10.);
#2523=VECTOR('',#15977,10.);
#2524=VECTOR('',#15978,10.);
#2525=VECTOR('',#15979,10.);
#2526=VECTOR('',#15986,10.);
#2527=VECTOR('',#15989,10.);
#2528=VECTOR('',#15990,10.);
#2529=VECTOR('',#15991,10.);
#2859=CYLINDRICAL_SURFACE('',#12629,0.999999999999975);
#2860=CYLINDRICAL_SURFACE('',#12634,1.99999999999998);
#2861=CYLINDRICAL_SURFACE('',#12638,0.500000000000007);
#2862=CYLINDRICAL_SURFACE('',#12641,0.499999999999998);
#2863=CYLINDRICAL_SURFACE('',#12646,0.999999999999975);
#2864=CYLINDRICAL_SURFACE('',#12651,1.99999999999998);
#2865=CYLINDRICAL_SURFACE('',#12655,0.500000000000007);
#2866=CYLINDRICAL_SURFACE('',#12659,0.499999999999998);
#2867=CYLINDRICAL_SURFACE('',#12665,0.999999999999981);
#2868=CYLINDRICAL_SURFACE('',#12669,0.999999999999967);
#2869=CYLINDRICAL_SURFACE('',#12675,1.99999999999997);
#2870=CYLINDRICAL_SURFACE('',#12679,1.99999999999998);
#2871=CYLINDRICAL_SURFACE('',#12683,0.999999999999981);
#2872=CYLINDRICAL_SURFACE('',#12687,0.999999999999967);
#2873=CYLINDRICAL_SURFACE('',#12693,1.99999999999997);
#2874=CYLINDRICAL_SURFACE('',#12697,1.99999999999998);
#2890=STYLED_ITEM('',(#19389),#107);
#3387=FACE_OUTER_BOUND('',#4446,.T.);
#3388=FACE_OUTER_BOUND('',#4447,.T.);
#3389=FACE_OUTER_BOUND('',#4448,.T.);
#3390=FACE_OUTER_BOUND('',#4449,.T.);
#3391=FACE_OUTER_BOUND('',#4450,.T.);
#3392=FACE_OUTER_BOUND('',#4451,.T.);
#3393=FACE_OUTER_BOUND('',#4452,.T.);
#3394=FACE_OUTER_BOUND('',#4453,.T.);
#3395=FACE_OUTER_BOUND('',#4454,.T.);
#3396=FACE_OUTER_BOUND('',#4455,.T.);
#3397=FACE_OUTER_BOUND('',#4456,.T.);
#3398=FACE_OUTER_BOUND('',#4457,.T.);
#3399=FACE_OUTER_BOUND('',#4458,.T.);
#3400=FACE_OUTER_BOUND('',#4459,.T.);
#3401=FACE_OUTER_BOUND('',#4460,.T.);
#3402=FACE_OUTER_BOUND('',#4461,.T.);
#3403=FACE_OUTER_BOUND('',#4462,.T.);
#3404=FACE_OUTER_BOUND('',#4463,.T.);
#3405=FACE_OUTER_BOUND('',#4464,.T.);
#3406=FACE_OUTER_BOUND('',#4465,.T.);
#3407=FACE_OUTER_BOUND('',#4466,.T.);
#3408=FACE_OUTER_BOUND('',#4467,.T.);
#3409=FACE_OUTER_BOUND('',#4468,.T.);
#3410=FACE_OUTER_BOUND('',#4469,.T.);
#3411=FACE_OUTER_BOUND('',#4470,.T.);
#3412=FACE_OUTER_BOUND('',#4471,.T.);
#3413=FACE_OUTER_BOUND('',#4472,.T.);
#3414=FACE_OUTER_BOUND('',#4473,.T.);
#3415=FACE_OUTER_BOUND('',#4474,.T.);
#3416=FACE_OUTER_BOUND('',#4475,.T.);
#3417=FACE_OUTER_BOUND('',#4476,.T.);
#3418=FACE_OUTER_BOUND('',#4477,.T.);
#3419=FACE_OUTER_BOUND('',#4478,.T.);
#3420=FACE_OUTER_BOUND('',#4479,.T.);
#3421=FACE_OUTER_BOUND('',#4480,.T.);
#3422=FACE_OUTER_BOUND('',#4481,.T.);
#3423=FACE_OUTER_BOUND('',#4482,.T.);
#3424=FACE_OUTER_BOUND('',#4483,.T.);
#3425=FACE_OUTER_BOUND('',#4484,.T.);
#3426=FACE_OUTER_BOUND('',#4485,.T.);
#3427=FACE_OUTER_BOUND('',#4486,.T.);
#3428=FACE_OUTER_BOUND('',#4488,.T.);
#4446=EDGE_LOOP('',(#10480,#10481,#10482,#10483));
#4447=EDGE_LOOP('',(#10484,#10485,#10486,#10487));
#4448=EDGE_LOOP('',(#10488,#10489,#10490,#10491));
#4449=EDGE_LOOP('',(#10492,#10493,#10494,#10495));
#4450=EDGE_LOOP('',(#10496,#10497,#10498,#10499));
#4451=EDGE_LOOP('',(#10500,#10501,#10502,#10503));
#4452=EDGE_LOOP('',(#10504,#10505,#10506,#10507));
#4453=EDGE_LOOP('',(#10508,#10509,#10510,#10511));
#4454=EDGE_LOOP('',(#10512,#10513,#10514,#10515));
#4455=EDGE_LOOP('',(#10516,#10517,#10518,#10519));
#4456=EDGE_LOOP('',(#10520,#10521,#10522,#10523));
#4457=EDGE_LOOP('',(#10524,#10525,#10526,#10527));
#4458=EDGE_LOOP('',(#10528,#10529,#10530,#10531));
#4459=EDGE_LOOP('',(#10532,#10533,#10534,#10535));
#4460=EDGE_LOOP('',(#10536,#10537,#10538,#10539));
#4461=EDGE_LOOP('',(#10540,#10541,#10542,#10543));
#4462=EDGE_LOOP('',(#10544,#10545,#10546,#10547));
#4463=EDGE_LOOP('',(#10548,#10549,#10550,#10551));
#4464=EDGE_LOOP('',(#10552,#10553,#10554,#10555));
#4465=EDGE_LOOP('',(#10556,#10557,#10558,#10559));
#4466=EDGE_LOOP('',(#10560,#10561,#10562,#10563));
#4467=EDGE_LOOP('',(#10564,#10565,#10566,#10567));
#4468=EDGE_LOOP('',(#10568,#10569,#10570,#10571));
#4469=EDGE_LOOP('',(#10572,#10573,#10574,#10575));
#4470=EDGE_LOOP('',(#10576,#10577,#10578,#10579));
#4471=EDGE_LOOP('',(#10580,#10581,#10582,#10583));
#4472=EDGE_LOOP('',(#10584,#10585,#10586,#10587));
#4473=EDGE_LOOP('',(#10588,#10589,#10590,#10591));
#4474=EDGE_LOOP('',(#10592,#10593,#10594,#10595));
#4475=EDGE_LOOP('',(#10596,#10597,#10598,#10599));
#4476=EDGE_LOOP('',(#10600,#10601,#10602,#10603));
#4477=EDGE_LOOP('',(#10604,#10605,#10606,#10607));
#4478=EDGE_LOOP('',(#10608,#10609,#10610,#10611));
#4479=EDGE_LOOP('',(#10612,#10613,#10614,#10615));
#4480=EDGE_LOOP('',(#10616,#10617,#10618,#10619));
#4481=EDGE_LOOP('',(#10620,#10621,#10622,#10623));
#4482=EDGE_LOOP('',(#10624,#10625,#10626,#10627));
#4483=EDGE_LOOP('',(#10628,#10629,#10630,#10631));
#4484=EDGE_LOOP('',(#10632,#10633,#10634,#10635));
#4485=EDGE_LOOP('',(#10636,#10637,#10638,#10639));
#4486=EDGE_LOOP('',(#10640,#10641,#10642,#10643,#10644,#10645,#10646,#10647,
#10648,#10649,#10650,#10651,#10652,#10653,#10654,#10655,#10656,#10657,#10658,
#10659,#10660,#10661,#10662,#10663,#10664,#10665,#10666,#10667,#10668,#10669));
#4487=EDGE_LOOP('',(#10670,#10671,#10672,#10673,#10674,#10675,#10676,#10677,
#10678,#10679));
#4488=EDGE_LOOP('',(#10680,#10681,#10682,#10683,#10684,#10685,#10686,#10687,
#10688,#10689,#10690,#10691,#10692,#10693,#10694,#10695,#10696,#10697,#10698,
#10699,#10700,#10701,#10702,#10703,#10704,#10705,#10706,#10707,#10708,#10709));
#4489=EDGE_LOOP('',(#10710,#10711,#10712,#10713,#10714,#10715,#10716,#10717,
#10718,#10719));
#5137=CIRCLE('',#12630,0.999999999999975);
#5138=CIRCLE('',#12631,0.999999999999975);
#5139=CIRCLE('',#12635,1.99999999999998);
#5140=CIRCLE('',#12636,1.99999999999998);
#5141=CIRCLE('',#12639,0.500000000000007);
#5142=CIRCLE('',#12640,0.500000000000007);
#5143=CIRCLE('',#12642,0.499999999999998);
#5144=CIRCLE('',#12643,0.499999999999998);
#5145=CIRCLE('',#12647,0.999999999999975);
#5146=CIRCLE('',#12648,0.999999999999975);
#5147=CIRCLE('',#12652,1.99999999999998);
#5148=CIRCLE('',#12653,1.99999999999998);
#5149=CIRCLE('',#12656,0.500000000000007);
#5150=CIRCLE('',#12657,0.500000000000007);
#5151=CIRCLE('',#12660,0.499999999999998);
#5152=CIRCLE('',#12661,0.499999999999998);
#5153=CIRCLE('',#12666,0.999999999999981);
#5154=CIRCLE('',#12667,0.999999999999981);
#5155=CIRCLE('',#12670,0.999999999999967);
#5156=CIRCLE('',#12671,0.999999999999967);
#5157=CIRCLE('',#12676,1.99999999999997);
#5158=CIRCLE('',#12677,1.99999999999997);
#5159=CIRCLE('',#12680,1.99999999999998);
#5160=CIRCLE('',#12681,1.99999999999998);
#5161=CIRCLE('',#12684,0.999999999999981);
#5162=CIRCLE('',#12685,0.999999999999981);
#5163=CIRCLE('',#12688,0.999999999999967);
#5164=CIRCLE('',#12689,0.999999999999967);
#5165=CIRCLE('',#12694,1.99999999999997);
#5166=CIRCLE('',#12695,1.99999999999997);
#5167=CIRCLE('',#12698,1.99999999999998);
#5168=CIRCLE('',#12699,1.99999999999998);
#6093=VERTEX_POINT('',#18889);
#6094=VERTEX_POINT('',#18890);
#6095=VERTEX_POINT('',#18892);
#6096=VERTEX_POINT('',#18894);
#6097=VERTEX_POINT('',#18898);
#6098=VERTEX_POINT('',#18900);
#6099=VERTEX_POINT('',#18904);
#6100=VERTEX_POINT('',#18906);
#6101=VERTEX_POINT('',#18910);
#6102=VERTEX_POINT('',#18911);
#6103=VERTEX_POINT('',#18913);
#6104=VERTEX_POINT('',#18915);
#6105=VERTEX_POINT('',#18919);
#6106=VERTEX_POINT('',#18921);
#6107=VERTEX_POINT('',#18925);
#6108=VERTEX_POINT('',#18927);
#6109=VERTEX_POINT('',#18931);
#6110=VERTEX_POINT('',#18933);
#6111=VERTEX_POINT('',#18937);
#6112=VERTEX_POINT('',#18939);
#6113=VERTEX_POINT('',#18943);
#6114=VERTEX_POINT('',#18945);
#6115=VERTEX_POINT('',#18949);
#6116=VERTEX_POINT('',#18950);
#6117=VERTEX_POINT('',#18952);
#6118=VERTEX_POINT('',#18954);
#6119=VERTEX_POINT('',#18958);
#6120=VERTEX_POINT('',#18960);
#6121=VERTEX_POINT('',#18964);
#6122=VERTEX_POINT('',#18966);
#6123=VERTEX_POINT('',#18970);
#6124=VERTEX_POINT('',#18971);
#6125=VERTEX_POINT('',#18973);
#6126=VERTEX_POINT('',#18975);
#6127=VERTEX_POINT('',#18979);
#6128=VERTEX_POINT('',#18981);
#6129=VERTEX_POINT('',#18985);
#6130=VERTEX_POINT('',#18987);
#6131=VERTEX_POINT('',#18994);
#6132=VERTEX_POINT('',#18996);
#6133=VERTEX_POINT('',#19003);
#6134=VERTEX_POINT('',#19005);
#6135=VERTEX_POINT('',#19009);
#6136=VERTEX_POINT('',#19011);
#6137=VERTEX_POINT('',#19018);
#6138=VERTEX_POINT('',#19020);
#6139=VERTEX_POINT('',#19024);
#6140=VERTEX_POINT('',#19026);
#6141=VERTEX_POINT('',#19030);
#6142=VERTEX_POINT('',#19032);
#6143=VERTEX_POINT('',#19036);
#6144=VERTEX_POINT('',#19038);
#6145=VERTEX_POINT('',#19042);
#6146=VERTEX_POINT('',#19044);
#6147=VERTEX_POINT('',#19048);
#6148=VERTEX_POINT('',#19050);
#6149=VERTEX_POINT('',#19054);
#6150=VERTEX_POINT('',#19056);
#6151=VERTEX_POINT('',#19060);
#6152=VERTEX_POINT('',#19062);
#6153=VERTEX_POINT('',#19066);
#6154=VERTEX_POINT('',#19068);
#6155=VERTEX_POINT('',#19072);
#6156=VERTEX_POINT('',#19074);
#6157=VERTEX_POINT('',#19078);
#6158=VERTEX_POINT('',#19080);
#6159=VERTEX_POINT('',#19084);
#6160=VERTEX_POINT('',#19086);
#6161=VERTEX_POINT('',#19090);
#6162=VERTEX_POINT('',#19092);
#6163=VERTEX_POINT('',#19096);
#6164=VERTEX_POINT('',#19098);
#6165=VERTEX_POINT('',#19102);
#6166=VERTEX_POINT('',#19104);
#6167=VERTEX_POINT('',#19108);
#6168=VERTEX_POINT('',#19110);
#6169=VERTEX_POINT('',#19114);
#6170=VERTEX_POINT('',#19116);
#6171=VERTEX_POINT('',#19120);
#6172=VERTEX_POINT('',#19122);
#7571=EDGE_CURVE('',#6093,#6094,#1587,.T.);
#7572=EDGE_CURVE('',#6094,#6095,#1588,.T.);
#7573=EDGE_CURVE('',#6095,#6096,#1589,.T.);
#7574=EDGE_CURVE('',#6093,#6096,#1590,.T.);
#7575=EDGE_CURVE('',#6097,#6094,#5137,.T.);
#7576=EDGE_CURVE('',#6097,#6098,#1591,.T.);
#7577=EDGE_CURVE('',#6098,#6095,#5138,.T.);
#7578=EDGE_CURVE('',#6097,#6099,#1592,.T.);
#7579=EDGE_CURVE('',#6100,#6099,#1593,.T.);
#7580=EDGE_CURVE('',#6100,#6098,#1594,.T.);
#7581=EDGE_CURVE('',#6101,#6102,#1595,.T.);
#7582=EDGE_CURVE('',#6101,#6103,#1596,.T.);
#7583=EDGE_CURVE('',#6103,#6104,#1597,.T.);
#7584=EDGE_CURVE('',#6102,#6104,#1598,.T.);
#7585=EDGE_CURVE('',#6101,#6105,#5139,.T.);
#7586=EDGE_CURVE('',#6105,#6106,#1599,.T.);
#7587=EDGE_CURVE('',#6106,#6103,#5140,.T.);
#7588=EDGE_CURVE('',#6107,#6105,#1600,.T.);
#7589=EDGE_CURVE('',#6107,#6108,#1601,.T.);
#7590=EDGE_CURVE('',#6108,#6106,#1602,.T.);
#7591=EDGE_CURVE('',#6109,#6107,#5141,.T.);
#7592=EDGE_CURVE('',#6109,#6110,#1603,.T.);
#7593=EDGE_CURVE('',#6110,#6108,#5142,.T.);
#7594=EDGE_CURVE('',#6111,#6093,#5143,.T.);
#7595=EDGE_CURVE('',#6096,#6112,#5144,.T.);
#7596=EDGE_CURVE('',#6111,#6112,#1604,.T.);
#7597=EDGE_CURVE('',#6109,#6113,#1605,.T.);
#7598=EDGE_CURVE('',#6113,#6114,#1606,.T.);
#7599=EDGE_CURVE('',#6114,#6110,#1607,.T.);
#7600=EDGE_CURVE('',#6115,#6116,#1608,.T.);
#7601=EDGE_CURVE('',#6115,#6117,#1609,.T.);
#7602=EDGE_CURVE('',#6118,#6117,#1610,.T.);
#7603=EDGE_CURVE('',#6116,#6118,#1611,.T.);
#7604=EDGE_CURVE('',#6119,#6116,#5145,.T.);
#7605=EDGE_CURVE('',#6120,#6118,#5146,.T.);
#7606=EDGE_CURVE('',#6119,#6120,#1612,.T.);
#7607=EDGE_CURVE('',#6119,#6121,#1613,.T.);
#7608=EDGE_CURVE('',#6122,#6120,#1614,.T.);
#7609=EDGE_CURVE('',#6121,#6122,#1615,.T.);
#7610=EDGE_CURVE('',#6123,#6124,#1616,.T.);
#7611=EDGE_CURVE('',#6125,#6124,#1617,.T.);
#7612=EDGE_CURVE('',#6126,#6125,#1618,.T.);
#7613=EDGE_CURVE('',#6123,#6126,#1619,.T.);
#7614=EDGE_CURVE('',#6123,#6127,#5147,.T.);
#7615=EDGE_CURVE('',#6128,#6126,#5148,.T.);
#7616=EDGE_CURVE('',#6127,#6128,#1620,.T.);
#7617=EDGE_CURVE('',#6129,#6127,#1621,.T.);
#7618=EDGE_CURVE('',#6130,#6128,#1622,.T.);
#7619=EDGE_CURVE('',#6129,#6130,#1623,.T.);
#7620=EDGE_CURVE('',#6113,#6129,#5149,.T.);
#7621=EDGE_CURVE('',#6114,#6130,#5150,.T.);
#7622=EDGE_CURVE('',#6131,#6112,#1624,.T.);
#7623=EDGE_CURVE('',#6132,#6131,#1625,.T.);
#7624=EDGE_CURVE('',#6111,#6132,#1626,.T.);
#7625=EDGE_CURVE('',#6132,#6115,#5151,.T.);
#7626=EDGE_CURVE('',#6117,#6131,#5152,.T.);
#7627=EDGE_CURVE('',#6133,#6122,#1627,.T.);
#7628=EDGE_CURVE('',#6134,#6133,#1628,.T.);
#7629=EDGE_CURVE('',#6134,#6121,#1629,.T.);
#7630=EDGE_CURVE('',#6099,#6135,#1630,.T.);
#7631=EDGE_CURVE('',#6135,#6136,#1631,.T.);
#7632=EDGE_CURVE('',#6100,#6136,#1632,.T.);
#7633=EDGE_CURVE('',#6125,#6104,#1633,.T.);
#7634=EDGE_CURVE('',#6124,#6102,#1634,.T.);
#7635=EDGE_CURVE('',#6137,#6135,#5153,.T.);
#7636=EDGE_CURVE('',#6137,#6138,#1635,.T.);
#7637=EDGE_CURVE('',#6138,#6136,#5154,.T.);
#7638=EDGE_CURVE('',#6137,#6139,#1636,.T.);
#7639=EDGE_CURVE('',#6139,#6140,#1637,.T.);
#7640=EDGE_CURVE('',#6140,#6138,#1638,.T.);
#7641=EDGE_CURVE('',#6141,#6139,#5155,.T.);
#7642=EDGE_CURVE('',#6141,#6142,#1639,.T.);
#7643=EDGE_CURVE('',#6142,#6140,#5156,.T.);
#7644=EDGE_CURVE('',#6141,#6143,#1640,.T.);
#7645=EDGE_CURVE('',#6143,#6144,#1641,.T.);
#7646=EDGE_CURVE('',#6144,#6142,#1642,.T.);
#7647=EDGE_CURVE('',#6145,#6143,#1643,.T.);
#7648=EDGE_CURVE('',#6145,#6146,#1644,.T.);
#7649=EDGE_CURVE('',#6146,#6144,#1645,.T.);
#7650=EDGE_CURVE('',#6147,#6145,#1646,.T.);
#7651=EDGE_CURVE('',#6147,#6148,#1647,.T.);
#7652=EDGE_CURVE('',#6148,#6146,#1648,.T.);
#7653=EDGE_CURVE('',#6147,#6149,#5157,.T.);
#7654=EDGE_CURVE('',#6149,#6150,#1649,.T.);
#7655=EDGE_CURVE('',#6150,#6148,#5158,.T.);
#7656=EDGE_CURVE('',#6151,#6149,#1650,.T.);
#7657=EDGE_CURVE('',#6151,#6152,#1651,.T.);
#7658=EDGE_CURVE('',#6152,#6150,#1652,.T.);
#7659=EDGE_CURVE('',#6151,#6153,#5159,.T.);
#7660=EDGE_CURVE('',#6153,#6154,#1653,.T.);
#7661=EDGE_CURVE('',#6154,#6152,#5160,.T.);
#7662=EDGE_CURVE('',#6153,#6155,#1654,.T.);
#7663=EDGE_CURVE('',#6155,#6156,#1655,.T.);
#7664=EDGE_CURVE('',#6156,#6154,#1656,.T.);
#7665=EDGE_CURVE('',#6157,#6134,#5161,.T.);
#7666=EDGE_CURVE('',#6158,#6133,#5162,.T.);
#7667=EDGE_CURVE('',#6157,#6158,#1657,.T.);
#7668=EDGE_CURVE('',#6157,#6159,#1658,.T.);
#7669=EDGE_CURVE('',#6160,#6158,#1659,.T.);
#7670=EDGE_CURVE('',#6159,#6160,#1660,.T.);
#7671=EDGE_CURVE('',#6161,#6159,#5163,.T.);
#7672=EDGE_CURVE('',#6162,#6160,#5164,.T.);
#7673=EDGE_CURVE('',#6161,#6162,#1661,.T.);
#7674=EDGE_CURVE('',#6161,#6163,#1662,.T.);
#7675=EDGE_CURVE('',#6164,#6162,#1663,.T.);
#7676=EDGE_CURVE('',#6163,#6164,#1664,.T.);
#7677=EDGE_CURVE('',#6165,#6163,#1665,.T.);
#7678=EDGE_CURVE('',#6166,#6164,#1666,.T.);
#7679=EDGE_CURVE('',#6165,#6166,#1667,.T.);
#7680=EDGE_CURVE('',#6167,#6165,#1668,.T.);
#7681=EDGE_CURVE('',#6168,#6166,#1669,.T.);
#7682=EDGE_CURVE('',#6167,#6168,#1670,.T.);
#7683=EDGE_CURVE('',#6167,#6169,#5165,.T.);
#7684=EDGE_CURVE('',#6170,#6168,#5166,.T.);
#7685=EDGE_CURVE('',#6169,#6170,#1671,.T.);
#7686=EDGE_CURVE('',#6171,#6169,#1672,.T.);
#7687=EDGE_CURVE('',#6172,#6170,#1673,.T.);
#7688=EDGE_CURVE('',#6171,#6172,#1674,.T.);
#7689=EDGE_CURVE('',#6171,#6155,#5167,.T.);
#7690=EDGE_CURVE('',#6156,#6172,#5168,.T.);
#10480=ORIENTED_EDGE('',*,*,#7571,.T.);
#10481=ORIENTED_EDGE('',*,*,#7572,.T.);
#10482=ORIENTED_EDGE('',*,*,#7573,.T.);
#10483=ORIENTED_EDGE('',*,*,#7574,.F.);
#10484=ORIENTED_EDGE('',*,*,#7575,.F.);
#10485=ORIENTED_EDGE('',*,*,#7576,.T.);
#10486=ORIENTED_EDGE('',*,*,#7577,.T.);
#10487=ORIENTED_EDGE('',*,*,#7572,.F.);
#10488=ORIENTED_EDGE('',*,*,#7578,.T.);
#10489=ORIENTED_EDGE('',*,*,#7579,.F.);
#10490=ORIENTED_EDGE('',*,*,#7580,.T.);
#10491=ORIENTED_EDGE('',*,*,#7576,.F.);
#10492=ORIENTED_EDGE('',*,*,#7581,.F.);
#10493=ORIENTED_EDGE('',*,*,#7582,.T.);
#10494=ORIENTED_EDGE('',*,*,#7583,.T.);
#10495=ORIENTED_EDGE('',*,*,#7584,.F.);
#10496=ORIENTED_EDGE('',*,*,#7585,.T.);
#10497=ORIENTED_EDGE('',*,*,#7586,.T.);
#10498=ORIENTED_EDGE('',*,*,#7587,.T.);
#10499=ORIENTED_EDGE('',*,*,#7582,.F.);
#10500=ORIENTED_EDGE('',*,*,#7588,.F.);
#10501=ORIENTED_EDGE('',*,*,#7589,.T.);
#10502=ORIENTED_EDGE('',*,*,#7590,.T.);
#10503=ORIENTED_EDGE('',*,*,#7586,.F.);
#10504=ORIENTED_EDGE('',*,*,#7591,.F.);
#10505=ORIENTED_EDGE('',*,*,#7592,.T.);
#10506=ORIENTED_EDGE('',*,*,#7593,.T.);
#10507=ORIENTED_EDGE('',*,*,#7589,.F.);
#10508=ORIENTED_EDGE('',*,*,#7594,.T.);
#10509=ORIENTED_EDGE('',*,*,#7574,.T.);
#10510=ORIENTED_EDGE('',*,*,#7595,.T.);
#10511=ORIENTED_EDGE('',*,*,#7596,.F.);
#10512=ORIENTED_EDGE('',*,*,#7597,.T.);
#10513=ORIENTED_EDGE('',*,*,#7598,.T.);
#10514=ORIENTED_EDGE('',*,*,#7599,.T.);
#10515=ORIENTED_EDGE('',*,*,#7592,.F.);
#10516=ORIENTED_EDGE('',*,*,#7600,.F.);
#10517=ORIENTED_EDGE('',*,*,#7601,.T.);
#10518=ORIENTED_EDGE('',*,*,#7602,.F.);
#10519=ORIENTED_EDGE('',*,*,#7603,.F.);
#10520=ORIENTED_EDGE('',*,*,#7604,.T.);
#10521=ORIENTED_EDGE('',*,*,#7603,.T.);
#10522=ORIENTED_EDGE('',*,*,#7605,.F.);
#10523=ORIENTED_EDGE('',*,*,#7606,.F.);
#10524=ORIENTED_EDGE('',*,*,#7607,.F.);
#10525=ORIENTED_EDGE('',*,*,#7606,.T.);
#10526=ORIENTED_EDGE('',*,*,#7608,.F.);
#10527=ORIENTED_EDGE('',*,*,#7609,.F.);
#10528=ORIENTED_EDGE('',*,*,#7610,.T.);
#10529=ORIENTED_EDGE('',*,*,#7611,.F.);
#10530=ORIENTED_EDGE('',*,*,#7612,.F.);
#10531=ORIENTED_EDGE('',*,*,#7613,.F.);
#10532=ORIENTED_EDGE('',*,*,#7614,.F.);
#10533=ORIENTED_EDGE('',*,*,#7613,.T.);
#10534=ORIENTED_EDGE('',*,*,#7615,.F.);
#10535=ORIENTED_EDGE('',*,*,#7616,.F.);
#10536=ORIENTED_EDGE('',*,*,#7617,.T.);
#10537=ORIENTED_EDGE('',*,*,#7616,.T.);
#10538=ORIENTED_EDGE('',*,*,#7618,.F.);
#10539=ORIENTED_EDGE('',*,*,#7619,.F.);
#10540=ORIENTED_EDGE('',*,*,#7620,.T.);
#10541=ORIENTED_EDGE('',*,*,#7619,.T.);
#10542=ORIENTED_EDGE('',*,*,#7621,.F.);
#10543=ORIENTED_EDGE('',*,*,#7598,.F.);
#10544=ORIENTED_EDGE('',*,*,#7622,.F.);
#10545=ORIENTED_EDGE('',*,*,#7623,.F.);
#10546=ORIENTED_EDGE('',*,*,#7624,.F.);
#10547=ORIENTED_EDGE('',*,*,#7596,.T.);
#10548=ORIENTED_EDGE('',*,*,#7625,.F.);
#10549=ORIENTED_EDGE('',*,*,#7623,.T.);
#10550=ORIENTED_EDGE('',*,*,#7626,.F.);
#10551=ORIENTED_EDGE('',*,*,#7601,.F.);
#10552=ORIENTED_EDGE('',*,*,#7609,.T.);
#10553=ORIENTED_EDGE('',*,*,#7627,.F.);
#10554=ORIENTED_EDGE('',*,*,#7628,.F.);
#10555=ORIENTED_EDGE('',*,*,#7629,.T.);
#10556=ORIENTED_EDGE('',*,*,#7579,.T.);
#10557=ORIENTED_EDGE('',*,*,#7630,.T.);
#10558=ORIENTED_EDGE('',*,*,#7631,.T.);
#10559=ORIENTED_EDGE('',*,*,#7632,.F.);
#10560=ORIENTED_EDGE('',*,*,#7584,.T.);
#10561=ORIENTED_EDGE('',*,*,#7633,.F.);
#10562=ORIENTED_EDGE('',*,*,#7611,.T.);
#10563=ORIENTED_EDGE('',*,*,#7634,.T.);
#10564=ORIENTED_EDGE('',*,*,#7635,.F.);
#10565=ORIENTED_EDGE('',*,*,#7636,.T.);
#10566=ORIENTED_EDGE('',*,*,#7637,.T.);
#10567=ORIENTED_EDGE('',*,*,#7631,.F.);
#10568=ORIENTED_EDGE('',*,*,#7638,.T.);
#10569=ORIENTED_EDGE('',*,*,#7639,.T.);
#10570=ORIENTED_EDGE('',*,*,#7640,.T.);
#10571=ORIENTED_EDGE('',*,*,#7636,.F.);
#10572=ORIENTED_EDGE('',*,*,#7641,.F.);
#10573=ORIENTED_EDGE('',*,*,#7642,.T.);
#10574=ORIENTED_EDGE('',*,*,#7643,.T.);
#10575=ORIENTED_EDGE('',*,*,#7639,.F.);
#10576=ORIENTED_EDGE('',*,*,#7644,.T.);
#10577=ORIENTED_EDGE('',*,*,#7645,.T.);
#10578=ORIENTED_EDGE('',*,*,#7646,.T.);
#10579=ORIENTED_EDGE('',*,*,#7642,.F.);
#10580=ORIENTED_EDGE('',*,*,#7647,.F.);
#10581=ORIENTED_EDGE('',*,*,#7648,.T.);
#10582=ORIENTED_EDGE('',*,*,#7649,.T.);
#10583=ORIENTED_EDGE('',*,*,#7645,.F.);
#10584=ORIENTED_EDGE('',*,*,#7650,.F.);
#10585=ORIENTED_EDGE('',*,*,#7651,.T.);
#10586=ORIENTED_EDGE('',*,*,#7652,.T.);
#10587=ORIENTED_EDGE('',*,*,#7648,.F.);
#10588=ORIENTED_EDGE('',*,*,#7653,.T.);
#10589=ORIENTED_EDGE('',*,*,#7654,.T.);
#10590=ORIENTED_EDGE('',*,*,#7655,.T.);
#10591=ORIENTED_EDGE('',*,*,#7651,.F.);
#10592=ORIENTED_EDGE('',*,*,#7656,.F.);
#10593=ORIENTED_EDGE('',*,*,#7657,.T.);
#10594=ORIENTED_EDGE('',*,*,#7658,.T.);
#10595=ORIENTED_EDGE('',*,*,#7654,.F.);
#10596=ORIENTED_EDGE('',*,*,#7659,.T.);
#10597=ORIENTED_EDGE('',*,*,#7660,.T.);
#10598=ORIENTED_EDGE('',*,*,#7661,.T.);
#10599=ORIENTED_EDGE('',*,*,#7657,.F.);
#10600=ORIENTED_EDGE('',*,*,#7662,.T.);
#10601=ORIENTED_EDGE('',*,*,#7663,.T.);
#10602=ORIENTED_EDGE('',*,*,#7664,.T.);
#10603=ORIENTED_EDGE('',*,*,#7660,.F.);
#10604=ORIENTED_EDGE('',*,*,#7665,.T.);
#10605=ORIENTED_EDGE('',*,*,#7628,.T.);
#10606=ORIENTED_EDGE('',*,*,#7666,.F.);
#10607=ORIENTED_EDGE('',*,*,#7667,.F.);
#10608=ORIENTED_EDGE('',*,*,#7668,.F.);
#10609=ORIENTED_EDGE('',*,*,#7667,.T.);
#10610=ORIENTED_EDGE('',*,*,#7669,.F.);
#10611=ORIENTED_EDGE('',*,*,#7670,.F.);
#10612=ORIENTED_EDGE('',*,*,#7671,.T.);
#10613=ORIENTED_EDGE('',*,*,#7670,.T.);
#10614=ORIENTED_EDGE('',*,*,#7672,.F.);
#10615=ORIENTED_EDGE('',*,*,#7673,.F.);
#10616=ORIENTED_EDGE('',*,*,#7674,.F.);
#10617=ORIENTED_EDGE('',*,*,#7673,.T.);
#10618=ORIENTED_EDGE('',*,*,#7675,.F.);
#10619=ORIENTED_EDGE('',*,*,#7676,.F.);
#10620=ORIENTED_EDGE('',*,*,#7677,.T.);
#10621=ORIENTED_EDGE('',*,*,#7676,.T.);
#10622=ORIENTED_EDGE('',*,*,#7678,.F.);
#10623=ORIENTED_EDGE('',*,*,#7679,.F.);
#10624=ORIENTED_EDGE('',*,*,#7680,.T.);
#10625=ORIENTED_EDGE('',*,*,#7679,.T.);
#10626=ORIENTED_EDGE('',*,*,#7681,.F.);
#10627=ORIENTED_EDGE('',*,*,#7682,.F.);
#10628=ORIENTED_EDGE('',*,*,#7683,.F.);
#10629=ORIENTED_EDGE('',*,*,#7682,.T.);
#10630=ORIENTED_EDGE('',*,*,#7684,.F.);
#10631=ORIENTED_EDGE('',*,*,#7685,.F.);
#10632=ORIENTED_EDGE('',*,*,#7686,.T.);
#10633=ORIENTED_EDGE('',*,*,#7685,.T.);
#10634=ORIENTED_EDGE('',*,*,#7687,.F.);
#10635=ORIENTED_EDGE('',*,*,#7688,.F.);
#10636=ORIENTED_EDGE('',*,*,#7689,.F.);
#10637=ORIENTED_EDGE('',*,*,#7688,.T.);
#10638=ORIENTED_EDGE('',*,*,#7690,.F.);
#10639=ORIENTED_EDGE('',*,*,#7663,.F.);
#10640=ORIENTED_EDGE('',*,*,#7578,.F.);
#10641=ORIENTED_EDGE('',*,*,#7575,.T.);
#10642=ORIENTED_EDGE('',*,*,#7571,.F.);
#10643=ORIENTED_EDGE('',*,*,#7594,.F.);
#10644=ORIENTED_EDGE('',*,*,#7624,.T.);
#10645=ORIENTED_EDGE('',*,*,#7625,.T.);
#10646=ORIENTED_EDGE('',*,*,#7600,.T.);
#10647=ORIENTED_EDGE('',*,*,#7604,.F.);
#10648=ORIENTED_EDGE('',*,*,#7607,.T.);
#10649=ORIENTED_EDGE('',*,*,#7629,.F.);
#10650=ORIENTED_EDGE('',*,*,#7665,.F.);
#10651=ORIENTED_EDGE('',*,*,#7668,.T.);
#10652=ORIENTED_EDGE('',*,*,#7671,.F.);
#10653=ORIENTED_EDGE('',*,*,#7674,.T.);
#10654=ORIENTED_EDGE('',*,*,#7677,.F.);
#10655=ORIENTED_EDGE('',*,*,#7680,.F.);
#10656=ORIENTED_EDGE('',*,*,#7683,.T.);
#10657=ORIENTED_EDGE('',*,*,#7686,.F.);
#10658=ORIENTED_EDGE('',*,*,#7689,.T.);
#10659=ORIENTED_EDGE('',*,*,#7662,.F.);
#10660=ORIENTED_EDGE('',*,*,#7659,.F.);
#10661=ORIENTED_EDGE('',*,*,#7656,.T.);
#10662=ORIENTED_EDGE('',*,*,#7653,.F.);
#10663=ORIENTED_EDGE('',*,*,#7650,.T.);
#10664=ORIENTED_EDGE('',*,*,#7647,.T.);
#10665=ORIENTED_EDGE('',*,*,#7644,.F.);
#10666=ORIENTED_EDGE('',*,*,#7641,.T.);
#10667=ORIENTED_EDGE('',*,*,#7638,.F.);
#10668=ORIENTED_EDGE('',*,*,#7635,.T.);
#10669=ORIENTED_EDGE('',*,*,#7630,.F.);
#10670=ORIENTED_EDGE('',*,*,#7634,.F.);
#10671=ORIENTED_EDGE('',*,*,#7610,.F.);
#10672=ORIENTED_EDGE('',*,*,#7614,.T.);
#10673=ORIENTED_EDGE('',*,*,#7617,.F.);
#10674=ORIENTED_EDGE('',*,*,#7620,.F.);
#10675=ORIENTED_EDGE('',*,*,#7597,.F.);
#10676=ORIENTED_EDGE('',*,*,#7591,.T.);
#10677=ORIENTED_EDGE('',*,*,#7588,.T.);
#10678=ORIENTED_EDGE('',*,*,#7585,.F.);
#10679=ORIENTED_EDGE('',*,*,#7581,.T.);
#10680=ORIENTED_EDGE('',*,*,#7632,.T.);
#10681=ORIENTED_EDGE('',*,*,#7637,.F.);
#10682=ORIENTED_EDGE('',*,*,#7640,.F.);
#10683=ORIENTED_EDGE('',*,*,#7643,.F.);
#10684=ORIENTED_EDGE('',*,*,#7646,.F.);
#10685=ORIENTED_EDGE('',*,*,#7649,.F.);
#10686=ORIENTED_EDGE('',*,*,#7652,.F.);
#10687=ORIENTED_EDGE('',*,*,#7655,.F.);
#10688=ORIENTED_EDGE('',*,*,#7658,.F.);
#10689=ORIENTED_EDGE('',*,*,#7661,.F.);
#10690=ORIENTED_EDGE('',*,*,#7664,.F.);
#10691=ORIENTED_EDGE('',*,*,#7690,.T.);
#10692=ORIENTED_EDGE('',*,*,#7687,.T.);
#10693=ORIENTED_EDGE('',*,*,#7684,.T.);
#10694=ORIENTED_EDGE('',*,*,#7681,.T.);
#10695=ORIENTED_EDGE('',*,*,#7678,.T.);
#10696=ORIENTED_EDGE('',*,*,#7675,.T.);
#10697=ORIENTED_EDGE('',*,*,#7672,.T.);
#10698=ORIENTED_EDGE('',*,*,#7669,.T.);
#10699=ORIENTED_EDGE('',*,*,#7666,.T.);
#10700=ORIENTED_EDGE('',*,*,#7627,.T.);
#10701=ORIENTED_EDGE('',*,*,#7608,.T.);
#10702=ORIENTED_EDGE('',*,*,#7605,.T.);
#10703=ORIENTED_EDGE('',*,*,#7602,.T.);
#10704=ORIENTED_EDGE('',*,*,#7626,.T.);
#10705=ORIENTED_EDGE('',*,*,#7622,.T.);
#10706=ORIENTED_EDGE('',*,*,#7595,.F.);
#10707=ORIENTED_EDGE('',*,*,#7573,.F.);
#10708=ORIENTED_EDGE('',*,*,#7577,.F.);
#10709=ORIENTED_EDGE('',*,*,#7580,.F.);
#10710=ORIENTED_EDGE('',*,*,#7583,.F.);
#10711=ORIENTED_EDGE('',*,*,#7587,.F.);
#10712=ORIENTED_EDGE('',*,*,#7590,.F.);
#10713=ORIENTED_EDGE('',*,*,#7593,.F.);
#10714=ORIENTED_EDGE('',*,*,#7599,.F.);
#10715=ORIENTED_EDGE('',*,*,#7621,.T.);
#10716=ORIENTED_EDGE('',*,*,#7618,.T.);
#10717=ORIENTED_EDGE('',*,*,#7615,.T.);
#10718=ORIENTED_EDGE('',*,*,#7612,.T.);
#10719=ORIENTED_EDGE('',*,*,#7633,.T.);
#11263=ADVANCED_FACE('',(#3387),#805,.F.);
#11264=ADVANCED_FACE('',(#3388),#2859,.F.);
#11265=ADVANCED_FACE('',(#3389),#806,.F.);
#11266=ADVANCED_FACE('',(#3390),#807,.F.);
#11267=ADVANCED_FACE('',(#3391),#2860,.T.);
#11268=ADVANCED_FACE('',(#3392),#808,.F.);
#11269=ADVANCED_FACE('',(#3393),#2861,.F.);
#11270=ADVANCED_FACE('',(#3394),#2862,.T.);
#11271=ADVANCED_FACE('',(#3395),#809,.T.);
#11272=ADVANCED_FACE('',(#3396),#810,.T.);
#11273=ADVANCED_FACE('',(#3397),#2863,.F.);
#11274=ADVANCED_FACE('',(#3398),#811,.T.);
#11275=ADVANCED_FACE('',(#3399),#812,.T.);
#11276=ADVANCED_FACE('',(#3400),#2864,.T.);
#11277=ADVANCED_FACE('',(#3401),#813,.T.);
#11278=ADVANCED_FACE('',(#3402),#2865,.F.);
#11279=ADVANCED_FACE('',(#3403),#814,.T.);
#11280=ADVANCED_FACE('',(#3404),#2866,.T.);
#11281=ADVANCED_FACE('',(#3405),#815,.T.);
#11282=ADVANCED_FACE('',(#3406),#816,.T.);
#11283=ADVANCED_FACE('',(#3407),#817,.T.);
#11284=ADVANCED_FACE('',(#3408),#2867,.F.);
#11285=ADVANCED_FACE('',(#3409),#818,.F.);
#11286=ADVANCED_FACE('',(#3410),#2868,.F.);
#11287=ADVANCED_FACE('',(#3411),#819,.F.);
#11288=ADVANCED_FACE('',(#3412),#820,.F.);
#11289=ADVANCED_FACE('',(#3413),#821,.F.);
#11290=ADVANCED_FACE('',(#3414),#2869,.T.);
#11291=ADVANCED_FACE('',(#3415),#822,.F.);
#11292=ADVANCED_FACE('',(#3416),#2870,.T.);
#11293=ADVANCED_FACE('',(#3417),#823,.T.);
#11294=ADVANCED_FACE('',(#3418),#2871,.F.);
#11295=ADVANCED_FACE('',(#3419),#824,.T.);
#11296=ADVANCED_FACE('',(#3420),#2872,.F.);
#11297=ADVANCED_FACE('',(#3421),#825,.T.);
#11298=ADVANCED_FACE('',(#3422),#826,.T.);
#11299=ADVANCED_FACE('',(#3423),#827,.T.);
#11300=ADVANCED_FACE('',(#3424),#2873,.T.);
#11301=ADVANCED_FACE('',(#3425),#828,.T.);
#11302=ADVANCED_FACE('',(#3426),#2874,.T.);
#11303=ADVANCED_FACE('',(#3427,#622),#829,.T.);
#11304=ADVANCED_FACE('',(#3428,#623),#830,.F.);
#11326=CLOSED_SHELL('',(#11263,#11264,#11265,#11266,#11267,#11268,#11269,
#11270,#11271,#11272,#11273,#11274,#11275,#11276,#11277,#11278,#11279,#11280,
#11281,#11282,#11283,#11284,#11285,#11286,#11287,#11288,#11289,#11290,#11291,
#11292,#11293,#11294,#11295,#11296,#11297,#11298,#11299,#11300,#11301,#11302,
#11303,#11304));
#12627=AXIS2_PLACEMENT_3D('',#18887,#15764,#15765);
#12628=AXIS2_PLACEMENT_3D('',#18888,#15766,#15767);
#12629=AXIS2_PLACEMENT_3D('',#18897,#15772,#15773);
#12630=AXIS2_PLACEMENT_3D('',#18899,#15774,#15775);
#12631=AXIS2_PLACEMENT_3D('',#18902,#15777,#15778);
#12632=AXIS2_PLACEMENT_3D('',#18903,#15779,#15780);
#12633=AXIS2_PLACEMENT_3D('',#18909,#15784,#15785);
#12634=AXIS2_PLACEMENT_3D('',#18918,#15790,#15791);
#12635=AXIS2_PLACEMENT_3D('',#18920,#15792,#15793);
#12636=AXIS2_PLACEMENT_3D('',#18923,#15795,#15796);
#12637=AXIS2_PLACEMENT_3D('',#18924,#15797,#15798);
#12638=AXIS2_PLACEMENT_3D('',#18930,#15802,#15803);
#12639=AXIS2_PLACEMENT_3D('',#18932,#15804,#15805);
#12640=AXIS2_PLACEMENT_3D('',#18935,#15807,#15808);
#12641=AXIS2_PLACEMENT_3D('',#18936,#15809,#15810);
#12642=AXIS2_PLACEMENT_3D('',#18938,#15811,#15812);
#12643=AXIS2_PLACEMENT_3D('',#18940,#15813,#15814);
#12644=AXIS2_PLACEMENT_3D('',#18942,#15816,#15817);
#12645=AXIS2_PLACEMENT_3D('',#18948,#15821,#15822);
#12646=AXIS2_PLACEMENT_3D('',#18957,#15827,#15828);
#12647=AXIS2_PLACEMENT_3D('',#18959,#15829,#15830);
#12648=AXIS2_PLACEMENT_3D('',#18961,#15831,#15832);
#12649=AXIS2_PLACEMENT_3D('',#18963,#15834,#15835);
#12650=AXIS2_PLACEMENT_3D('',#18969,#15839,#15840);
#12651=AXIS2_PLACEMENT_3D('',#18978,#15845,#15846);
#12652=AXIS2_PLACEMENT_3D('',#18980,#15847,#15848);
#12653=AXIS2_PLACEMENT_3D('',#18982,#15849,#15850);
#12654=AXIS2_PLACEMENT_3D('',#18984,#15852,#15853);
#12655=AXIS2_PLACEMENT_3D('',#18990,#15857,#15858);
#12656=AXIS2_PLACEMENT_3D('',#18991,#15859,#15860);
#12657=AXIS2_PLACEMENT_3D('',#18992,#15861,#15862);
#12658=AXIS2_PLACEMENT_3D('',#18993,#15863,#15864);
#12659=AXIS2_PLACEMENT_3D('',#18999,#15868,#15869);
#12660=AXIS2_PLACEMENT_3D('',#19000,#15870,#15871);
#12661=AXIS2_PLACEMENT_3D('',#19001,#15872,#15873);
#12662=AXIS2_PLACEMENT_3D('',#19002,#15874,#15875);
#12663=AXIS2_PLACEMENT_3D('',#19008,#15879,#15880);
#12664=AXIS2_PLACEMENT_3D('',#19014,#15884,#15885);
#12665=AXIS2_PLACEMENT_3D('',#19017,#15888,#15889);
#12666=AXIS2_PLACEMENT_3D('',#19019,#15890,#15891);
#12667=AXIS2_PLACEMENT_3D('',#19022,#15893,#15894);
#12668=AXIS2_PLACEMENT_3D('',#19023,#15895,#15896);
#12669=AXIS2_PLACEMENT_3D('',#19029,#15900,#15901);
#12670=AXIS2_PLACEMENT_3D('',#19031,#15902,#15903);
#12671=AXIS2_PLACEMENT_3D('',#19034,#15905,#15906);
#12672=AXIS2_PLACEMENT_3D('',#19035,#15907,#15908);
#12673=AXIS2_PLACEMENT_3D('',#19041,#15912,#15913);
#12674=AXIS2_PLACEMENT_3D('',#19047,#15917,#15918);
#12675=AXIS2_PLACEMENT_3D('',#19053,#15922,#15923);
#12676=AXIS2_PLACEMENT_3D('',#19055,#15924,#15925);
#12677=AXIS2_PLACEMENT_3D('',#19058,#15927,#15928);
#12678=AXIS2_PLACEMENT_3D('',#19059,#15929,#15930);
#12679=AXIS2_PLACEMENT_3D('',#19065,#15934,#15935);
#12680=AXIS2_PLACEMENT_3D('',#19067,#15936,#15937);
#12681=AXIS2_PLACEMENT_3D('',#19070,#15939,#15940);
#12682=AXIS2_PLACEMENT_3D('',#19071,#15941,#15942);
#12683=AXIS2_PLACEMENT_3D('',#19077,#15946,#15947);
#12684=AXIS2_PLACEMENT_3D('',#19079,#15948,#15949);
#12685=AXIS2_PLACEMENT_3D('',#19081,#15950,#15951);
#12686=AXIS2_PLACEMENT_3D('',#19083,#15953,#15954);
#12687=AXIS2_PLACEMENT_3D('',#19089,#15958,#15959);
#12688=AXIS2_PLACEMENT_3D('',#19091,#15960,#15961);
#12689=AXIS2_PLACEMENT_3D('',#19093,#15962,#15963);
#12690=AXIS2_PLACEMENT_3D('',#19095,#15965,#15966);
#12691=AXIS2_PLACEMENT_3D('',#19101,#15970,#15971);
#12692=AXIS2_PLACEMENT_3D('',#19107,#15975,#15976);
#12693=AXIS2_PLACEMENT_3D('',#19113,#15980,#15981);
#12694=AXIS2_PLACEMENT_3D('',#19115,#15982,#15983);
#12695=AXIS2_PLACEMENT_3D('',#19117,#15984,#15985);
#12696=AXIS2_PLACEMENT_3D('',#19119,#15987,#15988);
#12697=AXIS2_PLACEMENT_3D('',#19125,#15992,#15993);
#12698=AXIS2_PLACEMENT_3D('',#19126,#15994,#15995);
#12699=AXIS2_PLACEMENT_3D('',#19127,#15996,#15997);
#12700=AXIS2_PLACEMENT_3D('',#19128,#15998,#15999);
#12701=AXIS2_PLACEMENT_3D('',#19129,#16000,#16001);
#15764=DIRECTION('axis',(0.,0.,1.));
#15765=DIRECTION('refdir',(1.,0.,0.));
#15766=DIRECTION('center_axis',(0.,-0.984725314960397,0.174115059877505));
#15767=DIRECTION('ref_axis',(0.,0.174115059877505,0.984725314960397));
#15768=DIRECTION('',(0.,-0.174115059877505,-0.984725314960397));
#15769=DIRECTION('',(-1.,0.,0.));
#15770=DIRECTION('',(0.,0.174115059877505,0.984725314960397));
#15771=DIRECTION('',(-1.,0.,0.));
#15772=DIRECTION('center_axis',(1.,0.,0.));
#15773=DIRECTION('ref_axis',(0.,-0.821913269381079,-0.569612655771715));
#15774=DIRECTION('center_axis',(-1.,0.,0.));
#15775=DIRECTION('ref_axis',(0.,-0.821913269381079,-0.569612655771715));
#15776=DIRECTION('',(-1.,0.,0.));
#15777=DIRECTION('center_axis',(-1.,0.,0.));
#15778=DIRECTION('ref_axis',(0.,-0.821913269381079,-0.569612655771715));
#15779=DIRECTION('center_axis',(0.,-0.821913269381085,-0.569612655771705));
#15780=DIRECTION('ref_axis',(0.,-0.569612655771705,0.821913269381085));
#15781=DIRECTION('',(0.,0.569612655771705,-0.821913269381085));
#15782=DIRECTION('',(1.,0.,0.));
#15783=DIRECTION('',(0.,-0.569612655771705,0.821913269381085));
#15784=DIRECTION('center_axis',(0.,0.821913269381085,0.569612655771706));
#15785=DIRECTION('ref_axis',(0.,0.569612655771706,-0.821913269381085));
#15786=DIRECTION('',(0.,0.569612655771706,-0.821913269381085));
#15787=DIRECTION('',(-1.,0.,0.));
#15788=DIRECTION('',(0.,0.569612655771706,-0.821913269381085));
#15789=DIRECTION('',(-1.,0.,0.));
#15790=DIRECTION('center_axis',(1.,0.,0.));
#15791=DIRECTION('ref_axis',(0.,-0.821913269381079,-0.569612655771714));
#15792=DIRECTION('center_axis',(-1.,0.,0.));
#15793=DIRECTION('ref_axis',(0.,-0.821913269381079,-0.569612655771714));
#15794=DIRECTION('',(-1.,0.,0.));
#15795=DIRECTION('center_axis',(1.,0.,0.));
#15796=DIRECTION('ref_axis',(0.,-0.821913269381079,-0.569612655771714));
#15797=DIRECTION('center_axis',(0.,0.984725314960397,-0.174115059877505));
#15798=DIRECTION('ref_axis',(0.,-0.174115059877505,-0.984725314960397));
#15799=DIRECTION('',(0.,-0.174115059877505,-0.984725314960397));
#15800=DIRECTION('',(-1.,0.,0.));
#15801=DIRECTION('',(0.,-0.174115059877505,-0.984725314960397));
#15802=DIRECTION('center_axis',(1.,0.,0.));
#15803=DIRECTION('ref_axis',(0.,8.88178419700113E-15,1.));
#15804=DIRECTION('center_axis',(-1.,0.,0.));
#15805=DIRECTION('ref_axis',(0.,8.88178419700113E-15,1.));
#15806=DIRECTION('',(-1.,0.,0.));
#15807=DIRECTION('center_axis',(-1.,0.,0.));
#15808=DIRECTION('ref_axis',(0.,8.88178419700113E-15,1.));
#15809=DIRECTION('center_axis',(1.,0.,0.));
#15810=DIRECTION('ref_axis',(0.,0.,1.));
#15811=DIRECTION('center_axis',(-1.,0.,0.));
#15812=DIRECTION('ref_axis',(0.,0.,1.));
#15813=DIRECTION('center_axis',(1.,0.,0.));
#15814=DIRECTION('ref_axis',(0.,0.,1.));
#15815=DIRECTION('',(-1.,0.,0.));
#15816=DIRECTION('center_axis',(0.,-6.91402766832813E-16,-1.));
#15817=DIRECTION('ref_axis',(0.,-1.,6.91402766832813E-16));
#15818=DIRECTION('',(0.,-1.,6.91402766832813E-16));
#15819=DIRECTION('',(-1.,0.,0.));
#15820=DIRECTION('',(0.,1.,6.91402766832813E-16));
#15821=DIRECTION('center_axis',(0.,-0.984725314960397,-0.174115059877505));
#15822=DIRECTION('ref_axis',(0.,-0.174115059877505,0.984725314960397));
#15823=DIRECTION('',(0.,0.174115059877505,-0.984725314960397));
#15824=DIRECTION('',(-1.,0.,0.));
#15825=DIRECTION('',(0.,-0.174115059877505,0.984725314960397));
#15826=DIRECTION('',(-1.,0.,0.));
#15827=DIRECTION('center_axis',(-1.,0.,0.));
#15828=DIRECTION('ref_axis',(0.,0.821913269381079,-0.569612655771715));
#15829=DIRECTION('center_axis',(1.,0.,0.));
#15830=DIRECTION('ref_axis',(0.,0.821913269381079,-0.569612655771715));
#15831=DIRECTION('center_axis',(1.,0.,0.));
#15832=DIRECTION('ref_axis',(0.,0.821913269381079,-0.569612655771715));
#15833=DIRECTION('',(-1.,0.,0.));
#15834=DIRECTION('center_axis',(0.,-0.821913269381085,0.569612655771705));
#15835=DIRECTION('ref_axis',(0.,0.569612655771705,0.821913269381085));
#15836=DIRECTION('',(0.,-0.569612655771705,-0.821913269381085));
#15837=DIRECTION('',(0.,0.569612655771705,0.821913269381085));
#15838=DIRECTION('',(-1.,0.,0.));
#15839=DIRECTION('center_axis',(0.,0.821913269381085,-0.569612655771706));
#15840=DIRECTION('ref_axis',(0.,-0.569612655771706,-0.821913269381085));
#15841=DIRECTION('',(0.,-0.569612655771706,-0.821913269381085));
#15842=DIRECTION('',(1.,0.,0.));
#15843=DIRECTION('',(0.,-0.569612655771706,-0.821913269381085));
#15844=DIRECTION('',(-1.,0.,0.));
#15845=DIRECTION('center_axis',(-1.,0.,0.));
#15846=DIRECTION('ref_axis',(0.,0.821913269381079,-0.569612655771714));
#15847=DIRECTION('center_axis',(1.,0.,0.));
#15848=DIRECTION('ref_axis',(0.,0.821913269381079,-0.569612655771714));
#15849=DIRECTION('center_axis',(-1.,0.,0.));
#15850=DIRECTION('ref_axis',(0.,0.821913269381079,-0.569612655771714));
#15851=DIRECTION('',(-1.,0.,0.));
#15852=DIRECTION('center_axis',(0.,0.984725314960397,0.174115059877505));
#15853=DIRECTION('ref_axis',(0.,0.174115059877505,-0.984725314960397));
#15854=DIRECTION('',(0.,0.174115059877505,-0.984725314960397));
#15855=DIRECTION('',(0.,0.174115059877505,-0.984725314960397));
#15856=DIRECTION('',(-1.,0.,0.));
#15857=DIRECTION('center_axis',(-1.,0.,0.));
#15858=DIRECTION('ref_axis',(0.,-8.88178419700113E-15,1.));
#15859=DIRECTION('center_axis',(1.,0.,0.));
#15860=DIRECTION('ref_axis',(0.,-8.88178419700113E-15,1.));
#15861=DIRECTION('center_axis',(1.,0.,0.));
#15862=DIRECTION('ref_axis',(0.,-8.88178419700113E-15,1.));
#15863=DIRECTION('center_axis',(0.,0.,1.));
#15864=DIRECTION('ref_axis',(0.,1.,0.));
#15865=DIRECTION('',(0.,1.,0.));
#15866=DIRECTION('',(-1.,0.,0.));
#15867=DIRECTION('',(0.,-1.,0.));
#15868=DIRECTION('center_axis',(-1.,0.,0.));
#15869=DIRECTION('ref_axis',(0.,0.,1.));
#15870=DIRECTION('center_axis',(1.,0.,0.));
#15871=DIRECTION('ref_axis',(0.,0.,1.));
#15872=DIRECTION('center_axis',(-1.,0.,0.));
#15873=DIRECTION('ref_axis',(0.,0.,1.));
#15874=DIRECTION('center_axis',(0.,0.,1.));
#15875=DIRECTION('ref_axis',(0.,1.,0.));
#15876=DIRECTION('',(0.,1.,0.));
#15877=DIRECTION('',(-1.,0.,0.));
#15878=DIRECTION('',(0.,1.,0.));
#15879=DIRECTION('center_axis',(0.,0.,1.));
#15880=DIRECTION('ref_axis',(0.,1.,0.));
#15881=DIRECTION('',(0.,1.,0.));
#15882=DIRECTION('',(-1.,0.,0.));
#15883=DIRECTION('',(0.,1.,0.));
#15884=DIRECTION('center_axis',(0.,0.,1.));
#15885=DIRECTION('ref_axis',(0.,1.,0.));
#15886=DIRECTION('',(0.,1.,0.));
#15887=DIRECTION('',(0.,1.,0.));
#15888=DIRECTION('center_axis',(1.,0.,0.));
#15889=DIRECTION('ref_axis',(0.,0.707106781186555,-0.70710678118654));
#15890=DIRECTION('center_axis',(-1.,0.,0.));
#15891=DIRECTION('ref_axis',(0.,0.707106781186555,-0.70710678118654));
#15892=DIRECTION('',(-1.,0.,0.));
#15893=DIRECTION('center_axis',(-1.,0.,0.));
#15894=DIRECTION('ref_axis',(0.,0.707106781186555,-0.70710678118654));
#15895=DIRECTION('center_axis',(0.,0.707106781186548,-0.707106781186548));
#15896=DIRECTION('ref_axis',(0.,-0.707106781186548,-0.707106781186548));
#15897=DIRECTION('',(0.,0.707106781186547,0.707106781186547));
#15898=DIRECTION('',(-1.,0.,0.));
#15899=DIRECTION('',(0.,-0.707106781186547,-0.707106781186547));
#15900=DIRECTION('center_axis',(1.,0.,0.));
#15901=DIRECTION('ref_axis',(0.,0.98480775301221,-0.17364817766692));
#15902=DIRECTION('center_axis',(-1.,0.,0.));
#15903=DIRECTION('ref_axis',(0.,0.98480775301221,-0.17364817766692));
#15904=DIRECTION('',(-1.,0.,0.));
#15905=DIRECTION('center_axis',(-1.,0.,0.));
#15906=DIRECTION('ref_axis',(0.,0.98480775301221,-0.17364817766692));
#15907=DIRECTION('center_axis',(0.,0.984807753012208,-0.173648177666932));
#15908=DIRECTION('ref_axis',(0.,-0.173648177666932,-0.984807753012208));
#15909=DIRECTION('',(0.,0.173648177666932,0.984807753012208));
#15910=DIRECTION('',(-1.,0.,0.));
#15911=DIRECTION('',(0.,-0.173648177666932,-0.984807753012208));
#15912=DIRECTION('center_axis',(0.,0.,-1.));
#15913=DIRECTION('ref_axis',(0.,-1.,0.));
#15914=DIRECTION('',(0.,-1.,0.));
#15915=DIRECTION('',(-1.,0.,0.));
#15916=DIRECTION('',(0.,-1.,0.));
#15917=DIRECTION('center_axis',(0.,-0.984807753012208,0.173648177666932));
#15918=DIRECTION('ref_axis',(0.,0.173648177666932,0.984807753012208));
#15919=DIRECTION('',(0.,0.173648177666932,0.984807753012208));
#15920=DIRECTION('',(-1.,0.,0.));
#15921=DIRECTION('',(0.,0.173648177666932,0.984807753012208));
#15922=DIRECTION('center_axis',(1.,0.,0.));
#15923=DIRECTION('ref_axis',(0.,0.984807753012209,-0.173648177666926));
#15924=DIRECTION('center_axis',(-1.,0.,0.));
#15925=DIRECTION('ref_axis',(0.,0.984807753012209,-0.173648177666926));
#15926=DIRECTION('',(-1.,0.,0.));
#15927=DIRECTION('center_axis',(1.,0.,0.));
#15928=DIRECTION('ref_axis',(0.,0.984807753012209,-0.173648177666926));
#15929=DIRECTION('center_axis',(0.,-0.707106781186547,0.707106781186548));
#15930=DIRECTION('ref_axis',(0.,0.707106781186548,0.707106781186547));
#15931=DIRECTION('',(0.,0.707106781186548,0.707106781186547));
#15932=DIRECTION('',(-1.,0.,0.));
#15933=DIRECTION('',(0.,0.707106781186548,0.707106781186547));
#15934=DIRECTION('center_axis',(1.,0.,0.));
#15935=DIRECTION('ref_axis',(0.,0.707106781186551,-0.707106781186544));
#15936=DIRECTION('center_axis',(-1.,0.,0.));
#15937=DIRECTION('ref_axis',(0.,0.707106781186551,-0.707106781186544));
#15938=DIRECTION('',(-1.,0.,0.));
#15939=DIRECTION('center_axis',(1.,0.,0.));
#15940=DIRECTION('ref_axis',(0.,0.707106781186551,-0.707106781186544));
#15941=DIRECTION('center_axis',(0.,0.,-1.));
#15942=DIRECTION('ref_axis',(0.,-1.,0.));
#15943=DIRECTION('',(0.,-1.,0.));
#15944=DIRECTION('',(-1.,0.,0.));
#15945=DIRECTION('',(0.,1.,0.));
#15946=DIRECTION('center_axis',(-1.,0.,0.));
#15947=DIRECTION('ref_axis',(0.,-0.707106781186555,-0.70710678118654));
#15948=DIRECTION('center_axis',(1.,0.,0.));
#15949=DIRECTION('ref_axis',(0.,-0.707106781186555,-0.70710678118654));
#15950=DIRECTION('center_axis',(1.,0.,0.));
#15951=DIRECTION('ref_axis',(0.,-0.707106781186555,-0.70710678118654));
#15952=DIRECTION('',(-1.,0.,0.));
#15953=DIRECTION('center_axis',(0.,0.707106781186548,0.707106781186548));
#15954=DIRECTION('ref_axis',(0.,0.707106781186548,-0.707106781186548));
#15955=DIRECTION('',(0.,-0.707106781186547,0.707106781186547));
#15956=DIRECTION('',(0.,0.707106781186547,-0.707106781186547));
#15957=DIRECTION('',(-1.,0.,0.));
#15958=DIRECTION('center_axis',(-1.,0.,0.));
#15959=DIRECTION('ref_axis',(0.,-0.98480775301221,-0.17364817766692));
#15960=DIRECTION('center_axis',(1.,0.,0.));
#15961=DIRECTION('ref_axis',(0.,-0.98480775301221,-0.17364817766692));
#15962=DIRECTION('center_axis',(1.,0.,0.));
#15963=DIRECTION('ref_axis',(0.,-0.98480775301221,-0.17364817766692));
#15964=DIRECTION('',(-1.,0.,0.));
#15965=DIRECTION('center_axis',(0.,0.984807753012208,0.173648177666932));
#15966=DIRECTION('ref_axis',(0.,0.173648177666932,-0.984807753012208));
#15967=DIRECTION('',(0.,-0.173648177666932,0.984807753012208));
#15968=DIRECTION('',(0.,0.173648177666932,-0.984807753012208));
#15969=DIRECTION('',(-1.,0.,0.));
#15970=DIRECTION('center_axis',(0.,0.,1.));
#15971=DIRECTION('ref_axis',(0.,1.,0.));
#15972=DIRECTION('',(0.,1.,0.));
#15973=DIRECTION('',(0.,1.,0.));
#15974=DIRECTION('',(-1.,0.,0.));
#15975=DIRECTION('center_axis',(0.,-0.984807753012208,-0.173648177666932));
#15976=DIRECTION('ref_axis',(0.,-0.173648177666932,0.984807753012208));
#15977=DIRECTION('',(0.,-0.173648177666932,0.984807753012208));
#15978=DIRECTION('',(0.,-0.173648177666932,0.984807753012208));
#15979=DIRECTION('',(-1.,0.,0.));
#15980=DIRECTION('center_axis',(-1.,0.,0.));
#15981=DIRECTION('ref_axis',(0.,-0.984807753012209,-0.173648177666926));
#15982=DIRECTION('center_axis',(1.,0.,0.));
#15983=DIRECTION('ref_axis',(0.,-0.984807753012209,-0.173648177666926));
#15984=DIRECTION('center_axis',(-1.,0.,0.));
#15985=DIRECTION('ref_axis',(0.,-0.984807753012209,-0.173648177666926));
#15986=DIRECTION('',(-1.,0.,0.));
#15987=DIRECTION('center_axis',(0.,-0.707106781186547,-0.707106781186548));
#15988=DIRECTION('ref_axis',(0.,-0.707106781186548,0.707106781186547));
#15989=DIRECTION('',(0.,-0.707106781186548,0.707106781186547));
#15990=DIRECTION('',(0.,-0.707106781186548,0.707106781186547));
#15991=DIRECTION('',(-1.,0.,0.));
#15992=DIRECTION('center_axis',(-1.,0.,0.));
#15993=DIRECTION('ref_axis',(0.,-0.707106781186551,-0.707106781186544));
#15994=DIRECTION('center_axis',(1.,0.,0.));
#15995=DIRECTION('ref_axis',(0.,-0.707106781186551,-0.707106781186544));
#15996=DIRECTION('center_axis',(-1.,0.,0.));
#15997=DIRECTION('ref_axis',(0.,-0.707106781186551,-0.707106781186544));
#15998=DIRECTION('center_axis',(1.,0.,0.));
#15999=DIRECTION('ref_axis',(0.,1.,0.));
#16000=DIRECTION('center_axis',(1.,0.,0.));
#16001=DIRECTION('ref_axis',(0.,1.,0.));
#18887=CARTESIAN_POINT('',(0.,0.,0.));
#18888=CARTESIAN_POINT('Origin',(384.,29.4811336906747,27.5456750096756));
#18889=CARTESIAN_POINT('',(384.,29.8952421751416,29.8877073880428));
#18890=CARTESIAN_POINT('',(384.,29.4811336906747,27.5456750096756));
#18891=CARTESIAN_POINT('',(384.,29.8952421751416,29.8877073880428));
#18892=CARTESIAN_POINT('',(47.9470000000001,29.4811336906747,27.5456750096756));
#18893=CARTESIAN_POINT('',(384.,29.4811336906747,27.5456750096756));
#18894=CARTESIAN_POINT('',(47.9470000000001,29.8952421751416,29.8877073880428));
#18895=CARTESIAN_POINT('',(47.9470000000001,29.8952421751416,29.8877073880428));
#18896=CARTESIAN_POINT('',(384.,29.8952421751416,29.8877073880428));
#18897=CARTESIAN_POINT('Origin',(384.,30.465859005635,27.3715599497981));
#18898=CARTESIAN_POINT('',(384.,29.643945736254,26.8019472940264));
#18899=CARTESIAN_POINT('Origin',(384.,30.465859005635,27.3715599497981));
#18900=CARTESIAN_POINT('',(47.9470000000001,29.643945736254,26.8019472940264));
#18901=CARTESIAN_POINT('',(384.,29.643945736254,26.8019472940264));
#18902=CARTESIAN_POINT('Origin',(47.9470000000001,30.465859005635,27.3715599497981));
#18903=CARTESIAN_POINT('Origin',(384.,31.5857864376269,24.));
#18904=CARTESIAN_POINT('',(384.,31.5857864376269,24.));
#18905=CARTESIAN_POINT('',(384.,29.643945736254,26.8019472940264));
#18906=CARTESIAN_POINT('',(47.9470000000001,31.5857864376269,24.));
#18907=CARTESIAN_POINT('',(384.,31.5857864376269,24.));
#18908=CARTESIAN_POINT('',(47.9470000000001,29.643945736254,26.8019472940264));
#18909=CARTESIAN_POINT('Origin',(384.,28.8220324668729,26.2323346382546));
#18910=CARTESIAN_POINT('',(384.,28.8220324668729,26.2323346382546));
#18911=CARTESIAN_POINT('',(384.,30.369113052182,24.));
#18912=CARTESIAN_POINT('',(384.,28.8220324668729,26.2323346382546));
#18913=CARTESIAN_POINT('',(47.9470000000001,28.8220324668729,26.2323346382546));
#18914=CARTESIAN_POINT('',(384.,28.8220324668729,26.2323346382546));
#18915=CARTESIAN_POINT('',(47.9470000000001,30.369113052182,24.));
#18916=CARTESIAN_POINT('',(47.9470000000001,28.8220324668729,26.2323346382546));
#18917=CARTESIAN_POINT('',(384.,30.369113052182,24.));
#18918=CARTESIAN_POINT('Origin',(384.,30.465859005635,27.3715599497981));
#18919=CARTESIAN_POINT('',(384.,28.4964083757143,27.7197900695531));
#18920=CARTESIAN_POINT('Origin',(384.,30.465859005635,27.3715599497981));
#18921=CARTESIAN_POINT('',(47.9470000000001,28.4964083757143,27.7197900695531));
#18922=CARTESIAN_POINT('',(384.,28.4964083757143,27.7197900695531));
#18923=CARTESIAN_POINT('Origin',(47.9470000000001,30.465859005635,27.3715599497981));
#18924=CARTESIAN_POINT('Origin',(384.,28.7029146884407,28.8877073880428));
#18925=CARTESIAN_POINT('',(384.,28.7029146884407,28.8877073880428));
#18926=CARTESIAN_POINT('',(384.,28.7029146884407,28.8877073880428));
#18927=CARTESIAN_POINT('',(47.9470000000001,28.7029146884407,28.8877073880428));
#18928=CARTESIAN_POINT('',(384.,28.7029146884407,28.8877073880428));
#18929=CARTESIAN_POINT('',(47.9470000000001,28.7029146884407,28.8877073880428));
#18930=CARTESIAN_POINT('Origin',(384.,28.2105520309605,28.9747649179816));
#18931=CARTESIAN_POINT('',(384.,28.2105520309605,29.4747649179816));
#18932=CARTESIAN_POINT('Origin',(384.,28.2105520309605,28.9747649179816));
#18933=CARTESIAN_POINT('',(47.9470000000001,28.2105520309605,29.4747649179816));
#18934=CARTESIAN_POINT('',(384.,28.2105520309605,29.4747649179816));
#18935=CARTESIAN_POINT('Origin',(47.9470000000001,28.2105520309605,28.9747649179816));
#18936=CARTESIAN_POINT('Origin',(384.,29.4028795176614,29.9747649179816));
#18937=CARTESIAN_POINT('',(384.,29.4028795176614,30.4747649179816));
#18938=CARTESIAN_POINT('Origin',(384.,29.4028795176614,29.9747649179816));
#18939=CARTESIAN_POINT('',(47.9470000000001,29.4028795176614,30.4747649179816));
#18940=CARTESIAN_POINT('Origin',(47.9470000000001,29.4028795176614,29.9747649179816));
#18941=CARTESIAN_POINT('',(384.,29.4028795176614,30.4747649179816));
#18942=CARTESIAN_POINT('Origin',(384.,25.0009567389882,29.4747649179816));
#18943=CARTESIAN_POINT('',(384.,21.7894479690395,29.4747649179816));
#18944=CARTESIAN_POINT('',(384.,25.0009567389882,29.4747649179816));
#18945=CARTESIAN_POINT('',(47.9470000000001,21.7894479690395,29.4747649179816));
#18946=CARTESIAN_POINT('',(384.,21.7894479690395,29.4747649179816));
#18947=CARTESIAN_POINT('',(47.9470000000001,24.9990432610118,29.4747649179816));
#18948=CARTESIAN_POINT('Origin',(384.,20.5188663093253,27.5456750096756));
#18949=CARTESIAN_POINT('',(384.,20.1047578248584,29.8877073880428));
#18950=CARTESIAN_POINT('',(384.,20.5188663093253,27.5456750096756));
#18951=CARTESIAN_POINT('',(384.,20.1047578248584,29.8877073880428));
#18952=CARTESIAN_POINT('',(47.9470000000001,20.1047578248584,29.8877073880428));
#18953=CARTESIAN_POINT('',(384.,20.1047578248584,29.8877073880428));
#18954=CARTESIAN_POINT('',(47.9470000000001,20.5188663093253,27.5456750096756));
#18955=CARTESIAN_POINT('',(47.9470000000001,20.1047578248584,29.8877073880428));
#18956=CARTESIAN_POINT('',(384.,20.5188663093253,27.5456750096756));
#18957=CARTESIAN_POINT('Origin',(384.,19.534140994365,27.3715599497981));
#18958=CARTESIAN_POINT('',(384.,20.356054263746,26.8019472940264));
#18959=CARTESIAN_POINT('Origin',(384.,19.534140994365,27.3715599497981));
#18960=CARTESIAN_POINT('',(47.9470000000001,20.356054263746,26.8019472940264));
#18961=CARTESIAN_POINT('Origin',(47.9470000000001,19.534140994365,27.3715599497981));
#18962=CARTESIAN_POINT('',(384.,20.356054263746,26.8019472940264));
#18963=CARTESIAN_POINT('Origin',(384.,18.4142135623731,24.));
#18964=CARTESIAN_POINT('',(384.,18.4142135623731,24.));
#18965=CARTESIAN_POINT('',(384.,20.356054263746,26.8019472940264));
#18966=CARTESIAN_POINT('',(47.9470000000001,18.4142135623731,24.));
#18967=CARTESIAN_POINT('',(47.9470000000001,20.356054263746,26.8019472940264));
#18968=CARTESIAN_POINT('',(384.,18.4142135623731,24.));
#18969=CARTESIAN_POINT('Origin',(384.,21.1779675331271,26.2323346382546));
#18970=CARTESIAN_POINT('',(384.,21.1779675331271,26.2323346382546));
#18971=CARTESIAN_POINT('',(384.,19.630886947818,24.));
#18972=CARTESIAN_POINT('',(384.,21.1779675331271,26.2323346382546));
#18973=CARTESIAN_POINT('',(47.9470000000001,19.630886947818,24.));
#18974=CARTESIAN_POINT('',(384.,19.630886947818,24.));
#18975=CARTESIAN_POINT('',(47.9470000000001,21.1779675331271,26.2323346382546));
#18976=CARTESIAN_POINT('',(47.9470000000001,21.1779675331271,26.2323346382546));
#18977=CARTESIAN_POINT('',(384.,21.1779675331271,26.2323346382546));
#18978=CARTESIAN_POINT('Origin',(384.,19.534140994365,27.3715599497981));
#18979=CARTESIAN_POINT('',(384.,21.5035916242857,27.7197900695531));
#18980=CARTESIAN_POINT('Origin',(384.,19.534140994365,27.3715599497981));
#18981=CARTESIAN_POINT('',(47.9470000000001,21.5035916242857,27.7197900695531));
#18982=CARTESIAN_POINT('Origin',(47.9470000000001,19.534140994365,27.3715599497981));
#18983=CARTESIAN_POINT('',(384.,21.5035916242857,27.7197900695531));
#18984=CARTESIAN_POINT('Origin',(384.,21.2970853115593,28.8877073880428));
#18985=CARTESIAN_POINT('',(384.,21.2970853115593,28.8877073880428));
#18986=CARTESIAN_POINT('',(384.,21.2970853115593,28.8877073880428));
#18987=CARTESIAN_POINT('',(47.9470000000001,21.2970853115593,28.8877073880428));
#18988=CARTESIAN_POINT('',(47.9470000000001,21.2970853115593,28.8877073880428));
#18989=CARTESIAN_POINT('',(384.,21.2970853115593,28.8877073880428));
#18990=CARTESIAN_POINT('Origin',(384.,21.7894479690395,28.9747649179816));
#18991=CARTESIAN_POINT('Origin',(384.,21.7894479690395,28.9747649179816));
#18992=CARTESIAN_POINT('Origin',(47.9470000000001,21.7894479690395,28.9747649179816));
#18993=CARTESIAN_POINT('Origin',(384.,20.5971204823386,30.4747649179816));
#18994=CARTESIAN_POINT('',(47.9470000000001,20.5971204823386,30.4747649179816));
#18995=CARTESIAN_POINT('',(47.9470000000001,25.0009567389882,30.4747649179816));
#18996=CARTESIAN_POINT('',(384.,20.5971204823386,30.4747649179816));
#18997=CARTESIAN_POINT('',(384.,20.5971204823386,30.4747649179816));
#18998=CARTESIAN_POINT('',(384.,25.0009567389882,30.4747649179816));
#18999=CARTESIAN_POINT('Origin',(384.,20.5971204823386,29.9747649179816));
#19000=CARTESIAN_POINT('Origin',(384.,20.5971204823386,29.9747649179816));
#19001=CARTESIAN_POINT('Origin',(47.9470000000001,20.5971204823386,29.9747649179816));
#19002=CARTESIAN_POINT('Origin',(384.,15.8284271247462,24.));
#19003=CARTESIAN_POINT('',(47.9470000000001,15.8284271247462,24.));
#19004=CARTESIAN_POINT('',(47.9470000000001,21.,24.));
#19005=CARTESIAN_POINT('',(384.,15.8284271247462,24.));
#19006=CARTESIAN_POINT('',(384.,15.8284271247462,24.));
#19007=CARTESIAN_POINT('',(384.,21.,24.));
#19008=CARTESIAN_POINT('Origin',(384.,15.8284271247462,24.));
#19009=CARTESIAN_POINT('',(384.,34.1715728752538,24.));
#19010=CARTESIAN_POINT('',(384.,21.,24.));
#19011=CARTESIAN_POINT('',(47.9470000000001,34.1715728752538,24.));
#19012=CARTESIAN_POINT('',(384.,34.1715728752538,24.));
#19013=CARTESIAN_POINT('',(47.9470000000001,21.,24.));
#19014=CARTESIAN_POINT('Origin',(384.,15.8284271247462,24.));
#19015=CARTESIAN_POINT('',(47.9470000000001,21.,24.));
#19016=CARTESIAN_POINT('',(384.,21.,24.));
#19017=CARTESIAN_POINT('Origin',(384.,34.1715728752538,25.));
#19018=CARTESIAN_POINT('',(384.,34.8786796564404,24.2928932188135));
#19019=CARTESIAN_POINT('Origin',(384.,34.1715728752538,25.));
#19020=CARTESIAN_POINT('',(47.9470000000001,34.8786796564404,24.2928932188135));
#19021=CARTESIAN_POINT('',(384.,34.8786796564404,24.2928932188135));
#19022=CARTESIAN_POINT('Origin',(47.9470000000001,34.1715728752538,25.));
#19023=CARTESIAN_POINT('Origin',(384.,37.3825273013137,26.7967408636868));
#19024=CARTESIAN_POINT('',(384.,37.3825273013137,26.7967408636868));
#19025=CARTESIAN_POINT('',(384.,34.8786796564404,24.2928932188135));
#19026=CARTESIAN_POINT('',(47.9470000000001,37.3825273013137,26.7967408636868));
#19027=CARTESIAN_POINT('',(384.,37.3825273013137,26.7967408636868));
#19028=CARTESIAN_POINT('',(47.9470000000001,34.8786796564404,24.2928932188135));
#19029=CARTESIAN_POINT('Origin',(384.,36.6754205201272,27.5038476448734));
#19030=CARTESIAN_POINT('',(384.,37.6602282731394,27.3301994672064));
#19031=CARTESIAN_POINT('Origin',(384.,36.6754205201272,27.5038476448734));
#19032=CARTESIAN_POINT('',(47.9470000000001,37.6602282731394,27.3301994672064));
#19033=CARTESIAN_POINT('',(384.,37.6602282731394,27.3301994672064));
#19034=CARTESIAN_POINT('Origin',(47.9470000000001,36.6754205201272,27.5038476448734));
#19035=CARTESIAN_POINT('Origin',(384.,38.2147000047147,30.4747649179816));
#19036=CARTESIAN_POINT('',(384.,38.2147000047147,30.4747649179816));
#19037=CARTESIAN_POINT('',(384.,37.6602282731394,27.3301994672064));
#19038=CARTESIAN_POINT('',(47.9470000000001,38.2147000047147,30.4747649179816));
#19039=CARTESIAN_POINT('',(384.,38.2147000047147,30.4747649179816));
#19040=CARTESIAN_POINT('',(47.9470000000001,37.6602282731394,27.3301994672064));
#19041=CARTESIAN_POINT('Origin',(384.,39.2301266166005,30.4747649179816));
#19042=CARTESIAN_POINT('',(384.,39.2301266166005,30.4747649179816));
#19043=CARTESIAN_POINT('',(384.,39.2301266166005,30.4747649179816));
#19044=CARTESIAN_POINT('',(47.9470000000001,39.2301266166005,30.4747649179816));
#19045=CARTESIAN_POINT('',(384.,39.2301266166005,30.4747649179816));
#19046=CARTESIAN_POINT('',(47.9470000000001,39.2301266166005,30.4747649179816));
#19047=CARTESIAN_POINT('Origin',(384.,38.6450360261516,27.1565512895395));
#19048=CARTESIAN_POINT('',(384.,38.6450360261516,27.1565512895395));
#19049=CARTESIAN_POINT('',(384.,38.6450360261516,27.1565512895395));
#19050=CARTESIAN_POINT('',(47.9470000000001,38.6450360261516,27.1565512895395));
#19051=CARTESIAN_POINT('',(384.,38.6450360261516,27.1565512895395));
#19052=CARTESIAN_POINT('',(47.9470000000001,38.6450360261516,27.1565512895395));
#19053=CARTESIAN_POINT('Origin',(384.,36.6754205201272,27.5038476448734));
#19054=CARTESIAN_POINT('',(384.,38.0896340825003,26.0896340825003));
#19055=CARTESIAN_POINT('Origin',(384.,36.6754205201272,27.5038476448734));
#19056=CARTESIAN_POINT('',(47.9470000000001,38.0896340825003,26.0896340825003));
#19057=CARTESIAN_POINT('',(384.,38.0896340825003,26.0896340825003));
#19058=CARTESIAN_POINT('Origin',(47.9470000000001,36.6754205201272,27.5038476448734));
#19059=CARTESIAN_POINT('Origin',(384.,35.5857864376269,23.5857864376269));
#19060=CARTESIAN_POINT('',(384.,35.5857864376269,23.5857864376269));
#19061=CARTESIAN_POINT('',(384.,35.5857864376269,23.5857864376269));
#19062=CARTESIAN_POINT('',(47.9470000000001,35.5857864376269,23.5857864376269));
#19063=CARTESIAN_POINT('',(384.,35.5857864376269,23.5857864376269));
#19064=CARTESIAN_POINT('',(47.9470000000001,35.5857864376269,23.5857864376269));
#19065=CARTESIAN_POINT('Origin',(384.,34.1715728752538,25.));
#19066=CARTESIAN_POINT('',(384.,34.1715728752538,23.));
#19067=CARTESIAN_POINT('Origin',(384.,34.1715728752538,25.));
#19068=CARTESIAN_POINT('',(47.9470000000001,34.1715728752538,23.));
#19069=CARTESIAN_POINT('',(384.,34.1715728752538,23.));
#19070=CARTESIAN_POINT('Origin',(47.9470000000001,34.1715728752538,25.));
#19071=CARTESIAN_POINT('Origin',(384.,25.,23.));
#19072=CARTESIAN_POINT('',(384.,15.8284271247462,23.));
#19073=CARTESIAN_POINT('',(384.,25.,23.));
#19074=CARTESIAN_POINT('',(47.9470000000001,15.8284271247462,23.));
#19075=CARTESIAN_POINT('',(384.,15.8284271247462,23.));
#19076=CARTESIAN_POINT('',(47.9470000000001,25.,23.));
#19077=CARTESIAN_POINT('Origin',(384.,15.8284271247462,25.));
#19078=CARTESIAN_POINT('',(384.,15.1213203435596,24.2928932188135));
#19079=CARTESIAN_POINT('Origin',(384.,15.8284271247462,25.));
#19080=CARTESIAN_POINT('',(47.9470000000001,15.1213203435596,24.2928932188135));
#19081=CARTESIAN_POINT('Origin',(47.9470000000001,15.8284271247462,25.));
#19082=CARTESIAN_POINT('',(384.,15.1213203435596,24.2928932188135));
#19083=CARTESIAN_POINT('Origin',(384.,12.6174726986863,26.7967408636868));
#19084=CARTESIAN_POINT('',(384.,12.6174726986863,26.7967408636868));
#19085=CARTESIAN_POINT('',(384.,15.1213203435596,24.2928932188135));
#19086=CARTESIAN_POINT('',(47.9470000000001,12.6174726986863,26.7967408636868));
#19087=CARTESIAN_POINT('',(47.9470000000001,15.1213203435596,24.2928932188135));
#19088=CARTESIAN_POINT('',(384.,12.6174726986863,26.7967408636868));
#19089=CARTESIAN_POINT('Origin',(384.,13.3245794798728,27.5038476448734));
#19090=CARTESIAN_POINT('',(384.,12.3397717268606,27.3301994672064));
#19091=CARTESIAN_POINT('Origin',(384.,13.3245794798728,27.5038476448734));
#19092=CARTESIAN_POINT('',(47.9470000000001,12.3397717268606,27.3301994672064));
#19093=CARTESIAN_POINT('Origin',(47.9470000000001,13.3245794798728,27.5038476448734));
#19094=CARTESIAN_POINT('',(384.,12.3397717268606,27.3301994672064));
#19095=CARTESIAN_POINT('Origin',(384.,11.7852999952853,30.4747649179816));
#19096=CARTESIAN_POINT('',(384.,11.7852999952853,30.4747649179816));
#19097=CARTESIAN_POINT('',(384.,12.3397717268606,27.3301994672064));
#19098=CARTESIAN_POINT('',(47.9470000000001,11.7852999952853,30.4747649179816));
#19099=CARTESIAN_POINT('',(47.9470000000001,12.3397717268606,27.3301994672064));
#19100=CARTESIAN_POINT('',(384.,11.7852999952853,30.4747649179816));
#19101=CARTESIAN_POINT('Origin',(384.,10.7698733833995,30.4747649179816));
#19102=CARTESIAN_POINT('',(384.,10.7698733833995,30.4747649179816));
#19103=CARTESIAN_POINT('',(384.,10.7698733833995,30.4747649179816));
#19104=CARTESIAN_POINT('',(47.9470000000001,10.7698733833995,30.4747649179816));
#19105=CARTESIAN_POINT('',(47.9470000000001,10.7698733833995,30.4747649179816));
#19106=CARTESIAN_POINT('',(384.,10.7698733833995,30.4747649179816));
#19107=CARTESIAN_POINT('Origin',(384.,11.3549639738484,27.1565512895395));
#19108=CARTESIAN_POINT('',(384.,11.3549639738484,27.1565512895395));
#19109=CARTESIAN_POINT('',(384.,11.3549639738484,27.1565512895395));
#19110=CARTESIAN_POINT('',(47.9470000000001,11.3549639738484,27.1565512895395));
#19111=CARTESIAN_POINT('',(47.9470000000001,11.3549639738484,27.1565512895395));
#19112=CARTESIAN_POINT('',(384.,11.3549639738484,27.1565512895395));
#19113=CARTESIAN_POINT('Origin',(384.,13.3245794798728,27.5038476448734));
#19114=CARTESIAN_POINT('',(384.,11.9103659174997,26.0896340825003));
#19115=CARTESIAN_POINT('Origin',(384.,13.3245794798728,27.5038476448734));
#19116=CARTESIAN_POINT('',(47.9470000000001,11.9103659174997,26.0896340825003));
#19117=CARTESIAN_POINT('Origin',(47.9470000000001,13.3245794798728,27.5038476448734));
#19118=CARTESIAN_POINT('',(384.,11.9103659174997,26.0896340825003));
#19119=CARTESIAN_POINT('Origin',(384.,14.4142135623731,23.5857864376269));
#19120=CARTESIAN_POINT('',(384.,14.4142135623731,23.5857864376269));
#19121=CARTESIAN_POINT('',(384.,14.4142135623731,23.5857864376269));
#19122=CARTESIAN_POINT('',(47.9470000000001,14.4142135623731,23.5857864376269));
#19123=CARTESIAN_POINT('',(47.9470000000001,14.4142135623731,23.5857864376269));
#19124=CARTESIAN_POINT('',(384.,14.4142135623731,23.5857864376269));
#19125=CARTESIAN_POINT('Origin',(384.,15.8284271247462,25.));
#19126=CARTESIAN_POINT('Origin',(384.,15.8284271247462,25.));
#19127=CARTESIAN_POINT('Origin',(47.9470000000001,15.8284271247462,25.));
#19128=CARTESIAN_POINT('Origin',(384.,17.8849366916998,26.7373824589908));
#19129=CARTESIAN_POINT('Origin',(47.9470000000001,17.8849366916998,26.7373824589908));
#19202=UNCERTAINTY_MEASURE_WITH_UNIT(LENGTH_MEASURE(0.01),#19221,
'DISTANCE_ACCURACY_VALUE',
'Maximum model space distance between geometric entities at asserted c
onnectivities');
#19204=UNCERTAINTY_MEASURE_WITH_UNIT(LENGTH_MEASURE(0.01),#19221,
'DISTANCE_ACCURACY_VALUE',
'Maximum model space distance between geometric entities at asserted c
onnectivities');
#19218=(
GEOMETRIC_REPRESENTATION_CONTEXT(3)
GLOBAL_UNCERTAINTY_ASSIGNED_CONTEXT((#19202))
GLOBAL_UNIT_ASSIGNED_CONTEXT((#19221,#19223,#19224))
REPRESENTATION_CONTEXT('','3D')
);
#19220=(
GEOMETRIC_REPRESENTATION_CONTEXT(3)
GLOBAL_UNCERTAINTY_ASSIGNED_CONTEXT((#19204))
GLOBAL_UNIT_ASSIGNED_CONTEXT((#19221,#19223,#19224))
REPRESENTATION_CONTEXT('','3D')
);
#19221=(
LENGTH_UNIT()
NAMED_UNIT(*)
SI_UNIT(.MILLI.,.METRE.)
);
#19223=(
NAMED_UNIT(*)
PLANE_ANGLE_UNIT()
SI_UNIT($,.RADIAN.)
);
#19224=(
NAMED_UNIT(*)
SI_UNIT($,.STERADIAN.)
SOLID_ANGLE_UNIT()
);
#19238=SHAPE_DEFINITION_REPRESENTATION(#19253,#19282);
#19253=PRODUCT_DEFINITION_SHAPE('',$,#19298);
#19282=SHAPE_REPRESENTATION('',(#12627),#19218);
#19284=PRODUCT_DEFINITION_CONTEXT('part definition',#19331,'design');
#19298=PRODUCT_DEFINITION('Slider_02 (1)','Slider_02 (1)',#19313,#19284);
#19313=PRODUCT_DEFINITION_FORMATION('',$,#19346);
#19331=APPLICATION_CONTEXT(
'Core Data for Automotive Mechanical Design Process');
#19332=PRODUCT_CONTEXT('part definition',#19331,'mechanical');
#19346=PRODUCT('Slider_02 (1)','Slider_02 (1)',$,(#19332));
#19383=COLOUR_RGB('Light Blue',0.38,0.62,0.78);
#19384=FILL_AREA_STYLE_COLOUR('',#19383);
#19385=FILL_AREA_STYLE('',(#19384));
#19386=SURFACE_STYLE_FILL_AREA(#19385);
#19387=SURFACE_SIDE_STYLE('',(#19386));
#19388=SURFACE_STYLE_USAGE(.BOTH.,#19387);
#19389=PRESENTATION_STYLE_ASSIGNMENT((#19388));
ENDSEC;
END-ISO-10303-21;
